ISO-10303-21;
HEADER;
FILE_DESCRIPTION (('STEP AP214'),
    '1' );
FILE_NAME ('Input Shaft.step',
    '2026-09-30T12:41:04',
    ( '' ),
    ( '' ),
    'SwSTEP 2.0',
    'SolidWorks 2026',
    '' );
FILE_SCHEMA (( 'AUTOMOTIVE_DESIGN' ));
ENDSEC;

DATA;
#15=ORIENTED_EDGE ( 'NONE', *, *, #7786, .T. ) ;
#56=PLANE ( 'NONE',  #43244 ) ;
#63=CARTESIAN_POINT ( 'NONE',  ( -1.895993822078342774E-14, 1.063390998062931622E-14, -55.00000000000000000 ) ) ;
#115=CIRCLE ( 'NONE', #9512, 12.49999999999999645 ) ;
#148=CARTESIAN_POINT ( 'NONE',  ( -12.49999999999999645, 0.000000000000000000, 125.0000000000000000 ) ) ;
#156=EDGE_LOOP ( 'NONE', ( #423, #28551, #31287, #3442 ) ) ;
#166=DIRECTION ( 'NONE',  ( 0.000000000000000000, 0.000000000000000000, -1.000000000000000000 ) ) ;
#169=DIRECTION ( 'NONE',  ( 1.000000000000000000, 0.000000000000000000, 0.000000000000000000 ) ) ;
#170=EDGE_CURVE ( 'NONE', #39780, #42290, #34086, .T. ) ;
#207=AXIS2_PLACEMENT_3D ( 'NONE', #33978, #19292, #34217 ) ;
#261=DIRECTION ( 'NONE',  ( 1.000000000000000000, 0.000000000000000000, 0.000000000000000000 ) ) ;
#316=ORIENTED_EDGE ( 'NONE', *, *, #31067, .T. ) ;
#357=AXIS2_PLACEMENT_3D ( 'NONE', #6016, #12869, #17238 ) ;
#423=ORIENTED_EDGE ( 'NONE', *, *, #2653, .T. ) ;
#489=EDGE_CURVE ( 'NONE', #6953, #36450, #38933, .T. ) ;
#499=AXIS2_PLACEMENT_3D ( 'NONE', #29602, #44534, #40396 ) ;
#631=EDGE_LOOP ( 'NONE', ( #17363, #21113 ) ) ;
#634=ORIENTED_EDGE ( 'NONE', *, *, #31497, .F. ) ;
#649=ORIENTED_EDGE ( 'NONE', *, *, #42063, .F. ) ;
#671=CYLINDRICAL_SURFACE ( 'NONE', #3431, 12.49999999999999645 ) ;
#751=LINE ( 'NONE', #15941, #40255 ) ;
#753=CARTESIAN_POINT ( 'NONE',  ( 12.49999999999999645, 1.530808498934191127E-15, 125.0000000000000000 ) ) ;
#764=ORIENTED_EDGE ( 'NONE', *, *, #26987, .T. ) ;
#790=PLANE ( 'NONE',  #33904 ) ;
#830=CARTESIAN_POINT ( 'NONE',  ( 6.782329983125267248, 10.49999999999999645, -105.0000000000000000 ) ) ;
#997=CARTESIAN_POINT ( 'NONE',  ( -8.637688417678550223, 13.69818742750669749, -44.99999999999998579 ) ) ;
#1246=DIRECTION ( 'NONE',  ( 0.000000000000000000, 0.000000000000000000, 1.000000000000000000 ) ) ;
#1248=CARTESIAN_POINT ( 'NONE',  ( -6.170112525937310188, 10.87104923258429068, 125.0000000000000000 ) ) ;
#1249=AXIS2_PLACEMENT_3D ( 'NONE', #32536, #21027, #13697 ) ;
#1258=LINE ( 'NONE', #997, #32148 ) ;
#1259=DIRECTION ( 'NONE',  ( 1.000000000000000000, 0.000000000000000000, 0.000000000000000000 ) ) ;
#1260=AXIS2_PLACEMENT_3D ( 'NONE', #16246, #12806, #42175 ) ;
#1285=AXIS2_PLACEMENT_3D ( 'NONE', #2106, #31249, #17021 ) ;
#1326=DIRECTION ( 'NONE',  ( 0.000000000000000000, 0.000000000000000000, -1.000000000000000000 ) ) ;
#1336=EDGE_LOOP ( 'NONE', ( #24915, #24539, #28080, #17825 ) ) ;
#1389=DIRECTION ( 'NONE',  ( -0.000000000000000000, -0.000000000000000000, -1.000000000000000000 ) ) ;
#1394=ORIENTED_EDGE ( 'NONE', *, *, #24254, .F. ) ;
#1407=CARTESIAN_POINT ( 'NONE',  ( 11.59999999999999787, 1.420590287010929336E-15, 40.80000000000001847 ) ) ;
#1416=DIRECTION ( 'NONE',  ( 0.000000000000000000, 0.000000000000000000, 1.000000000000000000 ) ) ;
#1472=COLOUR_RGB ( '', 0.72549020, 0.75294118, 0.79215686) ;
#1473=LINE ( 'NONE', #39401, #40711 ) ;
#1594=VERTEX_POINT ( 'NONE', #19355 ) ;
#1636=EDGE_LOOP ( 'NONE', ( #13747, #42938, #25740, #19750 ) ) ;
#1692=VERTEX_POINT ( 'NONE', #46999 ) ;
#1716=ORIENTED_EDGE ( 'NONE', *, *, #22153, .T. ) ;
#1719=PLANE ( 'NONE',  #41597 ) ;
#1784=VERTEX_POINT ( 'NONE', #39674 ) ;
#1811=ORIENTED_EDGE ( 'NONE', *, *, #489, .T. ) ;
#1812=CARTESIAN_POINT ( 'NONE',  ( -9.332068499558253905, 6.890028847512361665, -54.99999999999998579 ) ) ;
#1820=ADVANCED_BREP_SHAPE_REPRESENTATION ( '', ( #35626, #11636 ), #3848 ) ;
#1971=ORIENTED_EDGE ( 'NONE', *, *, #16873, .T. ) ;
#2000=ADVANCED_FACE ( 'NONE', ( #34460 ), #34709, .T. ) ;
#2006=VECTOR ( 'NONE', #36863, 1000.000000000000114 ) ;
#2069=DIRECTION ( 'NONE',  ( 1.000000000000000000, 0.000000000000000000, 0.000000000000000000 ) ) ;
#2106=CARTESIAN_POINT ( 'NONE',  ( 0.000000000000000000, 0.000000000000000000, 125.0000000000000000 ) ) ;
#2192=CARTESIAN_POINT ( 'NONE',  ( 0.000000000000000000, 0.000000000000000000, 53.20000000000001705 ) ) ;
#2296=ORIENTED_EDGE ( 'NONE', *, *, #3696, .F. ) ;
#2465=ADVANCED_FACE ( 'NONE', ( #5778 ), #12882, .T. ) ;
#2488=CARTESIAN_POINT ( 'NONE',  ( 0.000000000000000000, 0.000000000000000000, 42.00000000000001421 ) ) ;
#2546=EDGE_LOOP ( 'NONE', ( #7119, #30843, #11967, #43447, #31695, #20805, #22594, #33669 ) ) ;
#2582=CIRCLE ( 'NONE', #41696, 12.49999999999999645 ) ;
#2595=ADVANCED_FACE ( 'NONE', ( #17747 ), #36348, .F. ) ;
#2616=VERTEX_POINT ( 'NONE', #13850 ) ;
#2653=EDGE_CURVE ( 'NONE', #14712, #46727, #6043, .T. ) ;
#2671=EDGE_LOOP ( 'NONE', ( #29337, #5818, #6491, #27847 ) ) ;
#2694=EDGE_CURVE ( 'NONE', #14256, #13625, #27143, .T. ) ;
#2712=DIRECTION ( 'NONE',  ( 1.000000000000000000, 0.000000000000000000, -0.000000000000000000 ) ) ;
#2782=SHAPE_REPRESENTATION ( 'Input Shaft', ( #11636 ), #3848 ) ;
#2806=DIRECTION ( 'NONE',  ( -0.000000000000000000, -0.000000000000000000, -1.000000000000000000 ) ) ;
#2842=ORIENTED_EDGE ( 'NONE', *, *, #20845, .T. ) ;
#2849=DIRECTION ( 'NONE',  ( 1.000000000000000000, 0.000000000000000000, 0.000000000000000000 ) ) ;
#2873=LINE ( 'NONE', #24680, #8806 ) ;
#2878=AXIS2_PLACEMENT_3D ( 'NONE', #44419, #6736, #25800 ) ;
#2905=EDGE_LOOP ( 'NONE', ( #41176, #10231, #43765, #2842, #45733, #45707, #47300, #38447 ) ) ;
#2980=DIRECTION ( 'NONE',  ( -1.000000000000000000, 0.000000000000000000, 0.000000000000000000 ) ) ;
#3048=DIRECTION ( 'NONE',  ( 0.6575728627325956310, -0.7533909544171997208, -1.230411769795008071E-16 ) ) ;
#3059=ADVANCED_FACE ( 'NONE', ( #3225 ), #18148, .T. ) ;
#3088=DIRECTION ( 'NONE',  ( 1.000000000000000000, 0.000000000000000000, 0.000000000000000000 ) ) ;
#3121=CARTESIAN_POINT ( 'NONE',  ( -6.170112525937322623, 10.87104923258428180, 125.0000000000000000 ) ) ;
#3142=CARTESIAN_POINT ( 'NONE',  ( 4.574237413256328308E-15, 3.992474787516289480E-15, 42.00000000000001421 ) ) ;
#3156=FACE_OUTER_BOUND ( 'NONE', #2671, .T. ) ;
#3159=CARTESIAN_POINT ( 'NONE',  ( 0.000000000000000000, 0.000000000000000000, 125.0000000000000000 ) ) ;
#3163=CARTESIAN_POINT ( 'NONE',  ( 0.000000000000000000, 0.000000000000000000, -56.19999999999998863 ) ) ;
#3191=EDGE_CURVE ( 'NONE', #45171, #17275, #16525, .T. ) ;
#3225=FACE_OUTER_BOUND ( 'NONE', #20798, .T. ) ;
#3241=DIRECTION ( 'NONE',  ( 0.6575728627325956310, -0.7533909544171996098, 0.000000000000000000 ) ) ;
#3277=CARTESIAN_POINT ( 'NONE',  ( -11.59999999999999787, 0.000000000000000000, 52.00000000000002132 ) ) ;
#3405=PLANE ( 'NONE',  #499 ) ;
#3412=( NAMED_UNIT ( * ) SI_UNIT ( $, .STERADIAN. ) SOLID_ANGLE_UNIT ( ) );
#3431=AXIS2_PLACEMENT_3D ( 'NONE', #11937, #3864, #38123 ) ;
#3442=ORIENTED_EDGE ( 'NONE', *, *, #48177, .F. ) ;
#3489=CARTESIAN_POINT ( 'NONE',  ( -8.637688417678527131, 13.69818742750669394, 42.00000000000001421 ) ) ;
#3566=DIRECTION ( 'NONE',  ( 1.000000000000000000, 0.000000000000000000, 0.000000000000000000 ) ) ;
#3579=CARTESIAN_POINT ( 'NONE',  ( -9.937067298023311679, 7.583184918921313411, 125.0000000000000000 ) ) ;
#3660=DIRECTION ( 'NONE',  ( 0.000000000000000000, -0.000000000000000000, 1.000000000000000000 ) ) ;
#3667=DIRECTION ( 'NONE',  ( 1.000000000000000000, 0.000000000000000000, 0.000000000000000000 ) ) ;
#3674=DIRECTION ( 'NONE',  ( -0.000000000000000000, -0.000000000000000000, -1.000000000000000000 ) ) ;
#3696=EDGE_CURVE ( 'NONE', #18977, #39357, #34908, .T. ) ;
#3697=CARTESIAN_POINT ( 'NONE',  ( -12.49999999999999645, 0.000000000000000000, 125.0000000000000000 ) ) ;
#3716=DIRECTION ( 'NONE',  ( -0.6575728627325955200, 0.7533909544171997208, 0.000000000000000000 ) ) ;
#3848=( GEOMETRIC_REPRESENTATION_CONTEXT ( 3 ) GLOBAL_UNCERTAINTY_ASSIGNED_CONTEXT ( ( #4164 ) ) GLOBAL_UNIT_ASSIGNED_CONTEXT ( ( #21552, #36230, #3412 ) ) REPRESENTATION_CONTEXT ( 'NONE', 'WORKASPACE' ) );
#3854=CARTESIAN_POINT ( 'NONE',  ( 0.000000000000000000, 0.000000000000000000, -43.79999999999998295 ) ) ;
#3864=DIRECTION ( 'NONE',  ( -0.000000000000000000, -0.000000000000000000, -1.000000000000000000 ) ) ;
#3865=ORIENTED_EDGE ( 'NONE', *, *, #24921, .T. ) ;
#3872=DIRECTION ( 'NONE',  ( 0.6575728627325957421, -0.7533909544171993877, -1.230411769795008318E-16 ) ) ;
#3987=CARTESIAN_POINT ( 'NONE',  ( -12.40464318976454727, 10.41032311384371845, -55.00000000000000000 ) ) ;
#4044=EDGE_LOOP ( 'NONE', ( #48070, #21337, #22064, #45180, #17709, #29362 ) ) ;
#4164=UNCERTAINTY_MEASURE_WITH_UNIT (LENGTH_MEASURE( 1.000000000000000082E-05 ), #21552, 'distance_accuracy_value', 'NONE');
#4212=CIRCLE ( 'NONE', #31576, 12.49999999999999645 ) ;
#4227=ADVANCED_FACE ( 'NONE', ( #17662 ), #21086, .T. ) ;
#4291=DIRECTION ( 'NONE',  ( -0.000000000000000000, -0.000000000000000000, -1.000000000000000000 ) ) ;
#4397=CARTESIAN_POINT ( 'NONE',  ( 0.000000000000000000, 0.000000000000000000, 125.0000000000000000 ) ) ;
#4441=LINE ( 'NONE', #8808, #27455 ) ;
#4453=LINE ( 'NONE', #753, #43424 ) ;
#4454=CARTESIAN_POINT ( 'NONE',  ( 0.000000000000000000, 0.000000000000000000, -43.79999999999998295 ) ) ;
#4477=ORIENTED_EDGE ( 'NONE', *, *, #5985, .T. ) ;
#4481=ORIENTED_EDGE ( 'NONE', *, *, #34973, .F. ) ;
#4494=LINE ( 'NONE', #31171, #4674 ) ;
#4519=AXIS2_PLACEMENT_3D ( 'NONE', #43355, #9556, #5916 ) ;
#4524=VERTEX_POINT ( 'NONE', #34505 ) ;
#4538=EDGE_CURVE ( 'NONE', #32290, #34023, #4441, .T. ) ;
#4598=CARTESIAN_POINT ( 'NONE',  ( -12.40464318976454727, 10.41032311384371667, -45.00000000000000000 ) ) ;
#4612=ORIENTED_EDGE ( 'NONE', *, *, #12889, .F. ) ;
#4674=VECTOR ( 'NONE', #30671, 1000.000000000000000 ) ;
#4679=DIRECTION ( 'NONE',  ( -0.000000000000000000, -0.000000000000000000, -1.000000000000000000 ) ) ;
#4690=EDGE_CURVE ( 'NONE', #19610, #31364, #48373, .T. ) ;
#4796=CARTESIAN_POINT ( 'NONE',  ( 12.49999999999999645, 1.530808498934191127E-15, -43.79999999999998295 ) ) ;
#4869=DIRECTION ( 'NONE',  ( 1.000000000000000000, 0.000000000000000000, 0.000000000000000000 ) ) ;
#4926=CARTESIAN_POINT ( 'NONE',  ( -12.49999999999999645, 0.000000000000000000, 125.0000000000000000 ) ) ;
#4936=VERTEX_POINT ( 'NONE', #28044 ) ;
#4980=EDGE_CURVE ( 'NONE', #9118, #34027, #19957, .T. ) ;
#4983=EDGE_CURVE ( 'NONE', #22767, #17326, #44600, .T. ) ;
#5091=ORIENTED_EDGE ( 'NONE', *, *, #170, .F. ) ;
#5134=DIRECTION ( 'NONE',  ( 0.000000000000000000, 0.000000000000000000, 1.000000000000000000 ) ) ;
#5150=EDGE_LOOP ( 'NONE', ( #39270, #4477, #48247, #16445 ) ) ;
#5176=DIRECTION ( 'NONE',  ( 0.6575728627325955200, -0.7533909544171996098, 0.000000000000000000 ) ) ;
#5377=EDGE_CURVE ( 'NONE', #6953, #14712, #31335, .T. ) ;
#5390=CARTESIAN_POINT ( 'NONE',  ( 11.59999999999999787, 1.420590287010929336E-15, 42.00000000000001421 ) ) ;
#5409=ORIENTED_EDGE ( 'NONE', *, *, #30554, .T. ) ;
#5468=AXIS2_PLACEMENT_3D ( 'NONE', #36465, #3660, #29600 ) ;
#5487=DIRECTION ( 'NONE',  ( -1.000000000000000000, 0.000000000000000000, 0.000000000000000000 ) ) ;
#5502=CYLINDRICAL_SURFACE ( 'NONE', #6275, 12.49999999999999645 ) ;
#5516=CYLINDRICAL_SURFACE ( 'NONE', #15981, 12.49999999999999645 ) ;
#5568=EDGE_LOOP ( 'NONE', ( #47034, #11080, #22029, #17339 ) ) ;
#5662=( LENGTH_UNIT ( ) NAMED_UNIT ( * ) SI_UNIT ( .MILLI., .METRE. ) );
#5675=AXIS2_PLACEMENT_3D ( 'NONE', #29049, #43981, #36631 ) ;
#5730=CARTESIAN_POINT ( 'NONE',  ( 0.000000000000000000, 0.000000000000000000, -43.79999999999998295 ) ) ;
#5747=EDGE_CURVE ( 'NONE', #9118, #21044, #37796, .T. ) ;
#5772=CARTESIAN_POINT ( 'NONE',  ( -3.702536634196095910, 8.043911037661889196, 42.00000000000001421 ) ) ;
#5778=FACE_OUTER_BOUND ( 'NONE', #5150, .T. ) ;
#5784=ORIENTED_EDGE ( 'NONE', *, *, #18304, .F. ) ;
#5790=DIRECTION ( 'NONE',  ( -1.000000000000000000, 0.000000000000000000, 0.000000000000000000 ) ) ;
#5800=AXIS2_PLACEMENT_3D ( 'NONE', #40812, #18289, #166 ) ;
#5810=DIRECTION ( 'NONE',  ( -1.000000000000000000, 0.000000000000000000, 0.000000000000000000 ) ) ;
#5818=ORIENTED_EDGE ( 'NONE', *, *, #35905, .F. ) ;
#5857=DIRECTION ( 'NONE',  ( 1.000000000000000000, 0.000000000000000000, 0.000000000000000000 ) ) ;
#5869=AXIS2_PLACEMENT_3D ( 'NONE', #10860, #18440, #29216 ) ;
#5916=DIRECTION ( 'NONE',  ( 1.000000000000000000, 0.000000000000000000, 0.000000000000000000 ) ) ;
#5923=DIRECTION ( 'NONE',  ( -0.7533909544171997208, -0.6575728627325955200, 0.000000000000000000 ) ) ;
#5982=DIRECTION ( 'NONE',  ( 0.000000000000000000, -0.000000000000000000, -1.000000000000000000 ) ) ;
#5985=EDGE_CURVE ( 'NONE', #14256, #1784, #22737, .T. ) ;
#5998=CIRCLE ( 'NONE', #40408, 12.49999999999999645 ) ;
#6005=DIRECTION ( 'NONE',  ( -1.000000000000000000, 0.000000000000000000, 0.000000000000000000 ) ) ;
#6016=CARTESIAN_POINT ( 'NONE',  ( 0.000000000000000000, 0.000000000000000000, 125.0000000000000000 ) ) ;
#6043=CIRCLE ( 'NONE', #2878, 11.59999999999999787 ) ;
#6118=DIRECTION ( 'NONE',  ( 0.000000000000000000, 0.000000000000000000, -1.000000000000000000 ) ) ;
#6142=SURFACE_STYLE_USAGE ( .BOTH. , #32568 ) ;
#6146=DIRECTION ( 'NONE',  ( 0.000000000000000000, 0.000000000000000000, 1.000000000000000000 ) ) ;
#6244=DIRECTION ( 'NONE',  ( 1.000000000000000000, 0.000000000000000000, -0.000000000000000000 ) ) ;
#6254=DIRECTION ( 'NONE',  ( 0.6575728627325955200, -0.7533909544171997208, 0.000000000000000000 ) ) ;
#6275=AXIS2_PLACEMENT_3D ( 'NONE', #27792, #42717, #6005 ) ;
#6329=CARTESIAN_POINT ( 'NONE',  ( 0.000000000000000000, 0.000000000000000000, -125.0000000000000000 ) ) ;
#6340=CIRCLE ( 'NONE', #46972, 12.49999999999999645 ) ;
#6362=EDGE_LOOP ( 'NONE', ( #16592, #33775, #7676, #27983 ) ) ;
#6469=EDGE_CURVE ( 'NONE', #7278, #16579, #23820, .T. ) ;
#6491=ORIENTED_EDGE ( 'NONE', *, *, #10060, .F. ) ;
#6524=LINE ( 'NONE', #37344, #17214 ) ;
#6561=AXIS2_PLACEMENT_3D ( 'NONE', #38454, #12753, #1259 ) ;
#6576=AXIS2_PLACEMENT_3D ( 'NONE', #21345, #24303, #14680 ) ;
#6619=DIRECTION ( 'NONE',  ( 0.000000000000000000, 0.000000000000000000, 1.000000000000000000 ) ) ;
#6631=ORIENTED_EDGE ( 'NONE', *, *, #34301, .T. ) ;
#6664=DIRECTION ( 'NONE',  ( 0.6575728627325957421, -0.7533909544171994987, 0.000000000000000000 ) ) ;
#6680=EDGE_LOOP ( 'NONE', ( #33457, #43610, #43331, #24165, #18798, #35762, #30907, #43194 ) ) ;
#6736=DIRECTION ( 'NONE',  ( 0.000000000000000000, 0.000000000000000000, 1.000000000000000000 ) ) ;
#6754=ORIENTED_EDGE ( 'NONE', *, *, #48050, .T. ) ;
#6755=ORIENTED_EDGE ( 'NONE', *, *, #19544, .T. ) ;
#6819=LINE ( 'NONE', #3121, #14420 ) ;
#6886=ORIENTED_EDGE ( 'NONE', *, *, #32944, .T. ) ;
#6925=AXIS2_PLACEMENT_3D ( 'NONE', #29189, #7159, #14999 ) ;
#6953=VERTEX_POINT ( 'NONE', #12293 ) ;
#6994=CARTESIAN_POINT ( 'NONE',  ( 0.000000000000000000, 0.000000000000000000, -44.99999999999998579 ) ) ;
#7050=EDGE_CURVE ( 'NONE', #7278, #44570, #46291, .T. ) ;
#7083=EDGE_CURVE ( 'NONE', #1594, #34027, #19939, .T. ) ;
#7119=ORIENTED_EDGE ( 'NONE', *, *, #24254, .T. ) ;
#7135=PLANE ( 'NONE',  #17794 ) ;
#7159=DIRECTION ( 'NONE',  ( 0.000000000000000000, 0.000000000000000000, 1.000000000000000000 ) ) ;
#7191=ORIENTED_EDGE ( 'NONE', *, *, #16873, .F. ) ;
#7238=DIRECTION ( 'NONE',  ( 8.090853898039828715E-17, -9.269810975720166919E-17, 1.000000000000000000 ) ) ;
#7245=CARTESIAN_POINT ( 'NONE',  ( -6.170112525937321735, 10.87104923258428180, -44.99999999999998579 ) ) ;
#7278=VERTEX_POINT ( 'NONE', #41362 ) ;
#7282=AXIS2_PLACEMENT_3D ( 'NONE', #20342, #16930, #8851 ) ;
#7335=SURFACE_SIDE_STYLE ('',( #47963 ) ) ;
#7373=ORIENTED_EDGE ( 'NONE', *, *, #48177, .T. ) ;
#7393=DIRECTION ( 'NONE',  ( 0.000000000000000000, 0.000000000000000000, -1.000000000000000000 ) ) ;
#7415=ORIENTED_EDGE ( 'NONE', *, *, #43885, .T. ) ;
#7502=CIRCLE ( 'NONE', #39560, 12.49999999999999645 ) ;
#7518=CARTESIAN_POINT ( 'NONE',  ( -6.170112525937308412, 10.87104923258428890, 52.00000000000002132 ) ) ;
#7609=VERTEX_POINT ( 'NONE', #46960 ) ;
#7676=ORIENTED_EDGE ( 'NONE', *, *, #40960, .T. ) ;
#7786=EDGE_CURVE ( 'NONE', #29688, #42999, #43910, .T. ) ;
#7894=AXIS2_PLACEMENT_3D ( 'NONE', #21103, #31923, #28464 ) ;
#7895=LINE ( 'NONE', #15729, #26909 ) ;
#7961=ORIENTED_EDGE ( 'NONE', *, *, #5377, .F. ) ;
#7995=EDGE_CURVE ( 'NONE', #17350, #15224, #38132, .T. ) ;
#8099=VERTEX_POINT ( 'NONE', #19742 ) ;
#8199=VERTEX_POINT ( 'NONE', #27597 ) ;
#8239=FACE_OUTER_BOUND ( 'NONE', #47849, .T. ) ;
#8326=VECTOR ( 'NONE', #43198, 1000.000000000000000 ) ;
#8536=ORIENTED_EDGE ( 'NONE', *, *, #15039, .T. ) ;
#8582=PRODUCT_DEFINITION_SHAPE ( 'NONE', 'NONE',  #16707 ) ;
#8640=AXIS2_PLACEMENT_3D ( 'NONE', #11049, #22316, #25720 ) ;
#8655=EDGE_CURVE ( 'NONE', #1692, #9518, #36632, .T. ) ;
#8691=CARTESIAN_POINT ( 'NONE',  ( 11.59999999999999787, 1.420590287010929336E-15, -54.99999999999998579 ) ) ;
#8771=DIRECTION ( 'NONE',  ( 1.000000000000000000, 0.000000000000000000, 0.000000000000000000 ) ) ;
#8806=VECTOR ( 'NONE', #43994, 1000.000000000000114 ) ;
#8808=CARTESIAN_POINT ( 'NONE',  ( -7.469491406282116941, 4.756046723998916370, -55.00000000000000000 ) ) ;
#8832=CARTESIAN_POINT ( 'NONE',  ( 0.000000000000000000, 0.000000000000000000, 42.00000000000001421 ) ) ;
#8851=DIRECTION ( 'NONE',  ( 1.000000000000000000, 0.000000000000000000, 0.000000000000000000 ) ) ;
#8880=VECTOR ( 'NONE', #38774, 1000.000000000000000 ) ;
#8924=CIRCLE ( 'NONE', #12098, 11.59999999999999787 ) ;
#8928=FACE_OUTER_BOUND ( 'NONE', #20534, .T. ) ;
#8945=FACE_OUTER_BOUND ( 'NONE', #4044, .T. ) ;
#9089=DIRECTION ( 'NONE',  ( 0.000000000000000000, 0.000000000000000000, 1.000000000000000000 ) ) ;
#9107=DIRECTION ( 'NONE',  ( 1.000000000000000000, 0.000000000000000000, 0.000000000000000000 ) ) ;
#9118=VERTEX_POINT ( 'NONE', #27247 ) ;
#9147=APPLICATION_CONTEXT ( 'automotive_design' ) ;
#9390=EDGE_CURVE ( 'NONE', #19610, #8099, #2582, .T. ) ;
#9512=AXIS2_PLACEMENT_3D ( 'NONE', #18527, #11910, #27562 ) ;
#9518=VERTEX_POINT ( 'NONE', #20018 ) ;
#9540=CIRCLE ( 'NONE', #47081, 12.49999999999999645 ) ;
#9556=DIRECTION ( 'NONE',  ( 0.000000000000000000, 0.000000000000000000, 1.000000000000000000 ) ) ;
#9715=ORIENTED_EDGE ( 'NONE', *, *, #44734, .F. ) ;
#9740=ORIENTED_EDGE ( 'NONE', *, *, #30395, .T. ) ;
#9812=EDGE_LOOP ( 'NONE', ( #44789, #21934 ) ) ;
#9885=VECTOR ( 'NONE', #15953, 1000.000000000000000 ) ;
#9887=ORIENTED_EDGE ( 'NONE', *, *, #41040, .T. ) ;
#9911=ADVANCED_FACE ( 'NONE', ( #8945 ), #19956, .F. ) ;
#9914=DIRECTION ( 'NONE',  ( -1.000000000000000000, 0.000000000000000000, 0.000000000000000000 ) ) ;
#9996=ORIENTED_EDGE ( 'NONE', *, *, #489, .F. ) ;
#10033=DIRECTION ( 'NONE',  ( 0.7533909544171996098, 0.6575728627325955200, -7.625282249115660656E-32 ) ) ;
#10048=AXIS2_PLACEMENT_3D ( 'NONE', #31223, #31956, #23615 ) ;
#10054=LINE ( 'NONE', #47720, #41684 ) ;
#10060=EDGE_CURVE ( 'NONE', #26557, #15072, #47583, .T. ) ;
#10082=DIRECTION ( 'NONE',  ( 0.000000000000000000, 0.000000000000000000, -1.000000000000000000 ) ) ;
#10101=CARTESIAN_POINT ( 'NONE',  ( -7.469491406282116941, 4.756046723998916370, -55.00000000000000000 ) ) ;
#10145=CARTESIAN_POINT ( 'NONE',  ( -3.702536634196120335, 8.043911037661892749, -55.00000000000000000 ) ) ;
#10186=EDGE_CURVE ( 'NONE', #26622, #46824, #33626, .T. ) ;
#10231=ORIENTED_EDGE ( 'NONE', *, *, #16460, .T. ) ;
#10247=AXIS2_PLACEMENT_3D ( 'NONE', #13949, #21766, #17365 ) ;
#10318=EDGE_LOOP ( 'NONE', ( #33965, #4481, #12484, #764 ) ) ;
#10405=DIRECTION ( 'NONE',  ( -0.6575728627325957421, 0.7533909544171994987, 0.000000000000000000 ) ) ;
#10507=DIRECTION ( 'NONE',  ( 0.000000000000000000, -0.000000000000000000, 1.000000000000000000 ) ) ;
#10509=ORIENTED_EDGE ( 'NONE', *, *, #4690, .T. ) ;
#10521=DIRECTION ( 'NONE',  ( 0.000000000000000000, 0.000000000000000000, 1.000000000000000000 ) ) ;
#10610=DIRECTION ( 'NONE',  ( 0.000000000000000000, 0.000000000000000000, 1.000000000000000000 ) ) ;
#10646=CARTESIAN_POINT ( 'NONE',  ( 0.000000000000000000, 0.000000000000000000, 42.00000000000001421 ) ) ;
#10656=CARTESIAN_POINT ( 'NONE',  ( -7.469491406282117829, 4.756046723998917258, -64.01812422950395387 ) ) ;
#10670=ADVANCED_FACE ( 'NONE', ( #37977 ), #48262, .T. ) ;
#10743=EDGE_CURVE ( 'NONE', #7609, #4936, #22760, .T. ) ;
#10785=CARTESIAN_POINT ( 'NONE',  ( -9.332068499558245023, 6.890028847512374988, 52.00000000000002132 ) ) ;
#10789=EDGE_CURVE ( 'NONE', #41629, #15072, #1258, .T. ) ;
#10860=CARTESIAN_POINT ( 'NONE',  ( 0.000000000000000000, 0.000000000000000000, -105.0000000000000000 ) ) ;
#10892=CARTESIAN_POINT ( 'NONE',  ( -12.40464318976452596, 10.41032311384371489, 42.00000000000001421 ) ) ;
#10984=EDGE_CURVE ( 'NONE', #12855, #43965, #45395, .T. ) ;
#10987=EDGE_CURVE ( 'NONE', #46304, #44570, #31389, .T. ) ;
#11049=CARTESIAN_POINT ( 'NONE',  ( 0.000000000000000000, 0.000000000000000000, 52.00000000000002132 ) ) ;
#11080=ORIENTED_EDGE ( 'NONE', *, *, #6469, .F. ) ;
#11107=PLANE ( 'NONE',  #23590 ) ;
#11192=DIRECTION ( 'NONE',  ( 0.000000000000000000, 0.000000000000000000, 1.000000000000000000 ) ) ;
#11195=CIRCLE ( 'NONE', #22114, 12.49999999999999645 ) ;
#11237=ORIENTED_EDGE ( 'NONE', *, *, #26934, .T. ) ;
#11375=AXIS2_PLACEMENT_3D ( 'NONE', #3163, #47486, #18094 ) ;
#11403=VECTOR ( 'NONE', #6118, 1000.000000000000000 ) ;
#11458=PLANE ( 'NONE',  #5800 ) ;
#11526=EDGE_LOOP ( 'NONE', ( #47076, #47499, #33440, #20776 ) ) ;
#11580=VECTOR ( 'NONE', #42086, 1000.000000000000000 ) ;
#11596=ADVANCED_FACE ( 'NONE', ( #22393 ), #37318, .T. ) ;
#11636=AXIS2_PLACEMENT_3D ( 'NONE', #13959, #6619, #3667 ) ;
#11853=DIRECTION ( 'NONE',  ( 0.000000000000000000, 0.000000000000000000, 1.000000000000000000 ) ) ;
#11910=DIRECTION ( 'NONE',  ( 0.000000000000000000, 0.000000000000000000, 1.000000000000000000 ) ) ;
#11937=CARTESIAN_POINT ( 'NONE',  ( 0.000000000000000000, 0.000000000000000000, 125.0000000000000000 ) ) ;
#11955=ORIENTED_EDGE ( 'NONE', *, *, #3191, .T. ) ;
#11959=VECTOR ( 'NONE', #18891, 1000.000000000000114 ) ;
#11967=ORIENTED_EDGE ( 'NONE', *, *, #5377, .T. ) ;
#12031=DIRECTION ( 'NONE',  ( 0.000000000000000000, 0.000000000000000000, 1.000000000000000000 ) ) ;
#12074=EDGE_CURVE ( 'NONE', #16579, #7278, #23262, .T. ) ;
#12098=AXIS2_PLACEMENT_3D ( 'NONE', #25641, #47445, #40583 ) ;
#12121=LINE ( 'NONE', #830, #33957 ) ;
#12162=CARTESIAN_POINT ( 'NONE',  ( 0.000000000000000000, 0.000000000000000000, 42.00000000000001421 ) ) ;
#12247=CARTESIAN_POINT ( 'NONE',  ( -5.565113727472241756, 10.17789316117534959, 42.00000000000001421 ) ) ;
#12273=AXIS2_PLACEMENT_3D ( 'NONE', #37795, #1326, #46605 ) ;
#12293=CARTESIAN_POINT ( 'NONE',  ( 11.59999999999999787, 1.420590287010929336E-15, 42.00000000000001421 ) ) ;
#12338=VERTEX_POINT ( 'NONE', #39571 ) ;
#12354=PLANE ( 'NONE',  #19348 ) ;
#12429=VECTOR ( 'NONE', #28975, 1000.000000000000000 ) ;
#12484=ORIENTED_EDGE ( 'NONE', *, *, #12655, .F. ) ;
#12603=AXIS2_PLACEMENT_3D ( 'NONE', #47479, #10521, #17852 ) ;
#12615=LINE ( 'NONE', #27542, #14161 ) ;
#12655=EDGE_CURVE ( 'NONE', #32749, #21372, #12121, .T. ) ;
#12714=ADVANCED_FACE ( 'NONE', ( #29977 ), #26313, .T. ) ;
#12717=ADVANCED_FACE ( 'NONE', ( #15532 ), #30466, .F. ) ;
#12753=DIRECTION ( 'NONE',  ( 0.000000000000000000, 0.000000000000000000, 1.000000000000000000 ) ) ;
#12806=DIRECTION ( 'NONE',  ( 0.000000000000000000, 0.000000000000000000, 1.000000000000000000 ) ) ;
#12807=AXIS2_PLACEMENT_3D ( 'NONE', #12871, #20686, #46883 ) ;
#12814=CARTESIAN_POINT ( 'NONE',  ( -11.59999999999999787, 0.000000000000000000, -54.99999999999998579 ) ) ;
#12855=VERTEX_POINT ( 'NONE', #1812 ) ;
#12869=DIRECTION ( 'NONE',  ( -0.000000000000000000, -0.000000000000000000, -1.000000000000000000 ) ) ;
#12871=CARTESIAN_POINT ( 'NONE',  ( -8.637688417678550223, 13.69818742750669749, -64.01812422950393966 ) ) ;
#12882=CYLINDRICAL_SURFACE ( 'NONE', #1285, 12.49999999999999645 ) ;
#12889=EDGE_CURVE ( 'NONE', #12338, #1784, #19119, .T. ) ;
#12958=CARTESIAN_POINT ( 'NONE',  ( 0.000000000000000000, 0.000000000000000000, 42.00000000000001421 ) ) ;
#13058=CARTESIAN_POINT ( 'NONE',  ( 0.000000000000000000, 0.000000000000000000, 42.00000000000001421 ) ) ;
#13120=DIRECTION ( 'NONE',  ( 0.000000000000000000, 0.000000000000000000, -1.000000000000000000 ) ) ;
#13216=CARTESIAN_POINT ( 'NONE',  ( 0.000000000000000000, 0.000000000000000000, 52.00000000000002132 ) ) ;
#13219=APPLICATION_CONTEXT ( 'automotive_design' ) ;
#13260=VECTOR ( 'NONE', #16822, 1000.000000000000000 ) ;
#13499=DIRECTION ( 'NONE',  ( 0.000000000000000000, 0.000000000000000000, 1.000000000000000000 ) ) ;
#13556=PLANE ( 'NONE',  #29963 ) ;
#13577=CARTESIAN_POINT ( 'NONE',  ( -7.469491406282094736, 4.756046723998911929, 52.00000000000002132 ) ) ;
#13582=CARTESIAN_POINT ( 'NONE',  ( 0.000000000000000000, 0.000000000000000000, 125.0000000000000000 ) ) ;
#13583=CARTESIAN_POINT ( 'NONE',  ( -8.637688417678548447, 13.69818742750669571, -45.00000000000000000 ) ) ;
#13590=CARTESIAN_POINT ( 'NONE',  ( -5.565113727472255967, 10.17789316117534248, -54.99999999999998579 ) ) ;
#13625=VERTEX_POINT ( 'NONE', #16812 ) ;
#13697=DIRECTION ( 'NONE',  ( 1.000000000000000000, 0.000000000000000000, 0.000000000000000000 ) ) ;
#13728=CARTESIAN_POINT ( 'NONE',  ( -6.782329983125267248, 10.49999999999999645, -125.0000000000000000 ) ) ;
#13747=ORIENTED_EDGE ( 'NONE', *, *, #20845, .F. ) ;
#13750=CARTESIAN_POINT ( 'NONE',  ( 0.000000000000000000, 0.000000000000000000, -43.79999999999998295 ) ) ;
#13850=CARTESIAN_POINT ( 'NONE',  ( -6.170112525937308412, 10.87104923258428890, 42.00000000000001421 ) ) ;
#13949=CARTESIAN_POINT ( 'NONE',  ( 0.000000000000000000, 0.000000000000000000, -125.0000000000000000 ) ) ;
#13959=CARTESIAN_POINT ( 'NONE',  ( 0.000000000000000000, 0.000000000000000000, 0.000000000000000000 ) ) ;
#13999=CARTESIAN_POINT ( 'NONE',  ( 0.000000000000000000, 0.000000000000000000, 53.20000000000001705 ) ) ;
#14000=ORIENTED_EDGE ( 'NONE', *, *, #30395, .F. ) ;
#14041=ADVANCED_FACE ( 'NONE', ( #17206 ), #39256, .T. ) ;
#14053=EDGE_CURVE ( 'NONE', #36450, #37662, #25224, .T. ) ;
#14099=VECTOR ( 'NONE', #6254, 1000.000000000000000 ) ;
#14126=FACE_OUTER_BOUND ( 'NONE', #19352, .T. ) ;
#14161=VECTOR ( 'NONE', #20421, 1000.000000000000000 ) ;
#14211=ADVANCED_FACE ( 'NONE', ( #33595 ), #56, .F. ) ;
#14222=CARTESIAN_POINT ( 'NONE',  ( -7.469491406282094736, 4.756046723998911929, 52.00000000000002132 ) ) ;
#14256=VERTEX_POINT ( 'NONE', #19860 ) ;
#14325=EDGE_LOOP ( 'NONE', ( #20378, #39933 ) ) ;
#14385=EDGE_CURVE ( 'NONE', #15224, #7609, #27638, .T. ) ;
#14394=DIRECTION ( 'NONE',  ( 0.000000000000000000, 0.000000000000000000, 1.000000000000000000 ) ) ;
#14420=VECTOR ( 'NONE', #36659, 1000.000000000000000 ) ;
#14426=EDGE_CURVE ( 'NONE', #27843, #26622, #31638, .T. ) ;
#14479=DIRECTION ( 'NONE',  ( 0.000000000000000000, 0.000000000000000000, 1.000000000000000000 ) ) ;
#14488=CIRCLE ( 'NONE', #5869, 12.49999999999999645 ) ;
#14504=FACE_OUTER_BOUND ( 'NONE', #29345, .T. ) ;
#14680=DIRECTION ( 'NONE',  ( 1.000000000000000000, 0.000000000000000000, 0.000000000000000000 ) ) ;
#14690=EDGE_LOOP ( 'NONE', ( #36188, #6631, #9740, #46262, #7191, #29753, #38485, #40889 ) ) ;
#14712=VERTEX_POINT ( 'NONE', #12247 ) ;
#14773=VECTOR ( 'NONE', #3872, 1000.000000000000114 ) ;
#14783=FACE_OUTER_BOUND ( 'NONE', #6680, .T. ) ;
#14853=CARTESIAN_POINT ( 'NONE',  ( -12.40464318976452596, 10.41032311384371489, 52.00000000000002132 ) ) ;
#14888=ORIENTED_EDGE ( 'NONE', *, *, #37714, .F. ) ;
#14999=DIRECTION ( 'NONE',  ( 1.000000000000000000, 0.000000000000000000, 0.000000000000000000 ) ) ;
#15006=CARTESIAN_POINT ( 'NONE',  ( -12.40464318976452596, 10.41032311384371489, 32.98187577049606745 ) ) ;
#15015=EDGE_CURVE ( 'NONE', #4524, #41629, #6819, .T. ) ;
#15039=EDGE_CURVE ( 'NONE', #46824, #40640, #8924, .T. ) ;
#15072=VERTEX_POINT ( 'NONE', #28839 ) ;
#15096=DIRECTION ( 'NONE',  ( -0.000000000000000000, -0.000000000000000000, -1.000000000000000000 ) ) ;
#15109=CARTESIAN_POINT ( 'NONE',  ( 0.000000000000000000, 0.000000000000000000, 125.0000000000000000 ) ) ;
#15118=ADVANCED_FACE ( 'NONE', ( #35100 ), #671, .T. ) ;
#15125=VERTEX_POINT ( 'NONE', #15603 ) ;
#15224=VERTEX_POINT ( 'NONE', #18551 ) ;
#15265=DIRECTION ( 'NONE',  ( 0.7533909544171996098, 0.6575728627325955200, -7.625282249115660656E-32 ) ) ;
#15313=ADVANCED_FACE ( 'NONE', ( #42703 ), #13556, .T. ) ;
#15323=CARTESIAN_POINT ( 'NONE',  ( -11.59999999999999787, 0.000000000000000000, 42.00000000000001421 ) ) ;
#15359=CARTESIAN_POINT ( 'NONE',  ( 0.000000000000000000, 0.000000000000000000, -56.19999999999998863 ) ) ;
#15412=CARTESIAN_POINT ( 'NONE',  ( 12.49999999999999645, 1.530808498934191127E-15, 125.0000000000000000 ) ) ;
#15448=DIRECTION ( 'NONE',  ( 1.000000000000000000, 0.000000000000000000, 0.000000000000000000 ) ) ;
#15475=CARTESIAN_POINT ( 'NONE',  ( 12.49999999999999645, 1.530808498934191127E-15, 40.80000000000001847 ) ) ;
#15532=FACE_OUTER_BOUND ( 'NONE', #10318, .T. ) ;
#15547=LINE ( 'NONE', #15323, #44912 ) ;
#15563=LINE ( 'NONE', #44225, #2006 ) ;
#15603=CARTESIAN_POINT ( 'NONE',  ( 12.49999999999999645, 1.530808498934191127E-15, -125.0000000000000000 ) ) ;
#15627=DIRECTION ( 'NONE',  ( 0.000000000000000000, 0.000000000000000000, 1.000000000000000000 ) ) ;
#15665=ORIENTED_EDGE ( 'NONE', *, *, #42046, .F. ) ;
#15688=EDGE_CURVE ( 'NONE', #39357, #42999, #22163, .T. ) ;
#15729=CARTESIAN_POINT ( 'NONE',  ( -9.937067298023318784, 7.583184918921300088, 125.0000000000000000 ) ) ;
#15738=CIRCLE ( 'NONE', #34487, 12.49999999999999645 ) ;
#15790=ADVANCED_FACE ( 'NONE', ( #44554, #21312 ), #47731, .T. ) ;
#15793=CARTESIAN_POINT ( 'NONE',  ( 12.49999999999999645, 1.530808498934191127E-15, -56.19999999999998863 ) ) ;
#15818=CARTESIAN_POINT ( 'NONE',  ( -7.469491406282116053, 4.756046723998915482, -45.00000000000000000 ) ) ;
#15828=LINE ( 'NONE', #34402, #46379 ) ;
#15897=EDGE_CURVE ( 'NONE', #15224, #19441, #21234, .T. ) ;
#15941=CARTESIAN_POINT ( 'NONE',  ( -7.469491406282094736, 4.756046723998911929, 32.98187577049606745 ) ) ;
#15953=DIRECTION ( 'NONE',  ( -0.000000000000000000, -0.000000000000000000, -1.000000000000000000 ) ) ;
#15981=AXIS2_PLACEMENT_3D ( 'NONE', #13582, #46645, #9914 ) ;
#16006=AXIS2_PLACEMENT_3D ( 'NONE', #37204, #3674, #18603 ) ;
#16035=ORIENTED_EDGE ( 'NONE', *, *, #5985, .F. ) ;
#16039=ADVANCED_FACE ( 'NONE', ( #44249 ), #11458, .F. ) ;
#16128=DIRECTION ( 'NONE',  ( 0.000000000000000000, 0.000000000000000000, 1.000000000000000000 ) ) ;
#16154=CARTESIAN_POINT ( 'NONE',  ( 0.000000000000000000, 0.000000000000000000, 52.00000000000002132 ) ) ;
#16162=ORIENTED_EDGE ( 'NONE', *, *, #39486, .T. ) ;
#16246=CARTESIAN_POINT ( 'NONE',  ( 0.000000000000000000, 0.000000000000000000, 52.00000000000002132 ) ) ;
#16372=CARTESIAN_POINT ( 'NONE',  ( -11.59999999999999787, 0.000000000000000000, 42.00000000000001421 ) ) ;
#16425=EDGE_CURVE ( 'NONE', #4936, #15072, #31663, .T. ) ;
#16445=ORIENTED_EDGE ( 'NONE', *, *, #26136, .F. ) ;
#16460=EDGE_CURVE ( 'NONE', #17350, #39780, #42586, .T. ) ;
#16462=VERTEX_POINT ( 'NONE', #29518 ) ;
#16477=AXIS2_PLACEMENT_3D ( 'NONE', #2192, #17828, #47677 ) ;
#16502=CARTESIAN_POINT ( 'NONE',  ( 0.000000000000000000, 0.000000000000000000, 40.80000000000001847 ) ) ;
#16525=CIRCLE ( 'NONE', #20422, 11.59999999999999787 ) ;
#16579=VERTEX_POINT ( 'NONE', #15793 ) ;
#16592=ORIENTED_EDGE ( 'NONE', *, *, #4538, .T. ) ;
#16632=VERTEX_POINT ( 'NONE', #19444 ) ;
#16656=ORIENTED_EDGE ( 'NONE', *, *, #15897, .T. ) ;
#16707=PRODUCT_DEFINITION ( 'UNKNOWN', '', #37413, #20840 ) ;
#16812=CARTESIAN_POINT ( 'NONE',  ( -12.49999999999999645, 0.000000000000000000, 125.0000000000000000 ) ) ;
#16822=DIRECTION ( 'NONE',  ( 0.000000000000000000, 0.000000000000000000, -1.000000000000000000 ) ) ;
#16827=DIRECTION ( 'NONE',  ( 1.000000000000000000, 0.000000000000000000, 0.000000000000000000 ) ) ;
#16836=ORIENTED_EDGE ( 'NONE', *, *, #21916, .T. ) ;
#16854=EDGE_LOOP ( 'NONE', ( #27017, #31852, #34991, #20358, #36187, #17761 ) ) ;
#16873=EDGE_CURVE ( 'NONE', #21372, #32749, #14488, .T. ) ;
#16930=DIRECTION ( 'NONE',  ( 0.000000000000000000, 0.000000000000000000, 1.000000000000000000 ) ) ;
#16960=DIRECTION ( 'NONE',  ( 1.000000000000000000, 0.000000000000000000, 0.000000000000000000 ) ) ;
#17021=DIRECTION ( 'NONE',  ( -1.000000000000000000, 0.000000000000000000, 0.000000000000000000 ) ) ;
#17032=CARTESIAN_POINT ( 'NONE',  ( 0.000000000000000000, 0.000000000000000000, 125.0000000000000000 ) ) ;
#17063=STYLED_ITEM ( 'NONE', ( #20831 ), #35626 ) ;
#17089=DIRECTION ( 'NONE',  ( 0.000000000000000000, 0.000000000000000000, 1.000000000000000000 ) ) ;
#17109=ORIENTED_EDGE ( 'NONE', *, *, #28524, .F. ) ;
#17146=( NAMED_UNIT ( * ) SI_UNIT ( $, .STERADIAN. ) SOLID_ANGLE_UNIT ( ) );
#17206=FACE_OUTER_BOUND ( 'NONE', #35234, .T. ) ;
#17214=VECTOR ( 'NONE', #7238, 1000.000000000000000 ) ;
#17238=DIRECTION ( 'NONE',  ( -1.000000000000000000, 0.000000000000000000, 0.000000000000000000 ) ) ;
#17275=VERTEX_POINT ( 'NONE', #21576 ) ;
#17305=AXIS2_PLACEMENT_3D ( 'NONE', #43683, #40018, #21402 ) ;
#17317=CARTESIAN_POINT ( 'NONE',  ( -12.40464318976454727, 10.41032311384371667, -45.00000000000000000 ) ) ;
#17326=VERTEX_POINT ( 'NONE', #29635 ) ;
#17339=ORIENTED_EDGE ( 'NONE', *, *, #47420, .T. ) ;
#17350=VERTEX_POINT ( 'NONE', #28907 ) ;
#17363=ORIENTED_EDGE ( 'NONE', *, *, #7083, .F. ) ;
#17365=DIRECTION ( 'NONE',  ( 1.000000000000000000, 0.000000000000000000, 0.000000000000000000 ) ) ;
#17485=FACE_OUTER_BOUND ( 'NONE', #27153, .T. ) ;
#17492=LINE ( 'NONE', #25314, #24633 ) ;
#17614=PLANE ( 'NONE',  #25359 ) ;
#17662=FACE_OUTER_BOUND ( 'NONE', #23970, .T. ) ;
#17668=CARTESIAN_POINT ( 'NONE',  ( -12.40464318976452596, 10.41032311384371489, 52.00000000000002132 ) ) ;
#17682=DIRECTION ( 'NONE',  ( -1.000000000000000000, 0.000000000000000000, 0.000000000000000000 ) ) ;
#17709=ORIENTED_EDGE ( 'NONE', *, *, #10789, .F. ) ;
#17727=EDGE_LOOP ( 'NONE', ( #15665, #32609, #42876, #6754, #30564, #38928, #35149, #34665 ) ) ;
#17747=FACE_OUTER_BOUND ( 'NONE', #6362, .T. ) ;
#17761=ORIENTED_EDGE ( 'NONE', *, *, #22083, .F. ) ;
#17794=AXIS2_PLACEMENT_3D ( 'NONE', #13999, #32600, #22054 ) ;
#17822=( GEOMETRIC_REPRESENTATION_CONTEXT ( 3 ) GLOBAL_UNCERTAINTY_ASSIGNED_CONTEXT ( ( #22749 ) ) GLOBAL_UNIT_ASSIGNED_CONTEXT ( ( #5662, #24496, #17146 ) ) REPRESENTATION_CONTEXT ( 'NONE', 'WORKASPACE' ) );
#17825=ORIENTED_EDGE ( 'NONE', *, *, #20163, .T. ) ;
#17828=DIRECTION ( 'NONE',  ( 0.000000000000000000, 0.000000000000000000, 1.000000000000000000 ) ) ;
#17852=DIRECTION ( 'NONE',  ( 1.000000000000000000, 0.000000000000000000, 0.000000000000000000 ) ) ;
#17995=AXIS2_PLACEMENT_3D ( 'NONE', #4454, #18868, #45307 ) ;
#18001=CARTESIAN_POINT ( 'NONE',  ( 0.000000000000000000, 0.000000000000000000, -44.99999999999998579 ) ) ;
#18025=CARTESIAN_POINT ( 'NONE',  ( 0.000000000000000000, 0.000000000000000000, -44.99999999999998579 ) ) ;
#18094=DIRECTION ( 'NONE',  ( 1.000000000000000000, 0.000000000000000000, 0.000000000000000000 ) ) ;
#18115=ORIENTED_EDGE ( 'NONE', *, *, #21054, .T. ) ;
#18132=FACE_BOUND ( 'NONE', #25467, .T. ) ;
#18148=CYLINDRICAL_SURFACE ( 'NONE', #25414, 11.59999999999999787 ) ;
#18151=AXIS2_PLACEMENT_3D ( 'NONE', #4397, #23221, #30333 ) ;
#18269=PLANE ( 'NONE',  #22800 ) ;
#18289=DIRECTION ( 'NONE',  ( 0.6575728627325954090, -0.7533909544171998318, 0.000000000000000000 ) ) ;
#18304=EDGE_CURVE ( 'NONE', #42290, #9518, #4494, .T. ) ;
#18320=AXIS2_PLACEMENT_3D ( 'NONE', #15359, #30285, #25860 ) ;
#18331=ORIENTED_EDGE ( 'NONE', *, *, #25661, .T. ) ;
#18353=SURFACE_STYLE_USAGE ( .BOTH. , #7335 ) ;
#18354=LINE ( 'NONE', #47713, #23274 ) ;
#18360=CYLINDRICAL_SURFACE ( 'NONE', #16006, 12.49999999999999645 ) ;
#18400=CYLINDRICAL_SURFACE ( 'NONE', #44866, 11.59999999999999787 ) ;
#18440=DIRECTION ( 'NONE',  ( -0.000000000000000000, 0.000000000000000000, -1.000000000000000000 ) ) ;
#18441=ADVANCED_FACE ( 'NONE', ( #43619 ), #21087, .T. ) ;
#18471=CARTESIAN_POINT ( 'NONE',  ( 0.000000000000000000, 0.000000000000000000, 125.0000000000000000 ) ) ;
#18513=DIRECTION ( 'NONE',  ( -0.000000000000000000, -0.000000000000000000, -1.000000000000000000 ) ) ;
#18527=CARTESIAN_POINT ( 'NONE',  ( 0.000000000000000000, 0.000000000000000000, 40.80000000000001847 ) ) ;
#18551=CARTESIAN_POINT ( 'NONE',  ( -9.332068499558252128, 6.890028847512362553, -44.99999999999998579 ) ) ;
#18598=PRESENTATION_STYLE_ASSIGNMENT (( #18353 ) ) ;
#18603=DIRECTION ( 'NONE',  ( -1.000000000000000000, 0.000000000000000000, 0.000000000000000000 ) ) ;
#18623=CARTESIAN_POINT ( 'NONE',  ( 0.000000000000000000, 0.000000000000000000, -44.99999999999998579 ) ) ;
#18624=DIRECTION ( 'NONE',  ( 0.000000000000000000, 0.000000000000000000, 1.000000000000000000 ) ) ;
#18711=EDGE_CURVE ( 'NONE', #8199, #27843, #43798, .T. ) ;
#18722=DIRECTION ( 'NONE',  ( 0.000000000000000000, 0.000000000000000000, -1.000000000000000000 ) ) ;
#18798=ORIENTED_EDGE ( 'NONE', *, *, #39486, .F. ) ;
#18809=CARTESIAN_POINT ( 'NONE',  ( 11.59999999999999787, 1.420590287010929336E-15, -43.79999999999998295 ) ) ;
#18868=DIRECTION ( 'NONE',  ( 0.000000000000000000, 0.000000000000000000, -1.000000000000000000 ) ) ;
#18891=DIRECTION ( 'NONE',  ( -0.6575728627325957421, 0.7533909544171993877, 1.230411769795008318E-16 ) ) ;
#18942=CARTESIAN_POINT ( 'NONE',  ( 0.000000000000000000, 0.000000000000000000, 125.0000000000000000 ) ) ;
#18977=VERTEX_POINT ( 'NONE', #43795 ) ;
#19022=CARTESIAN_POINT ( 'NONE',  ( -3.702536634196095910, 8.043911037661889196, 52.00000000000002132 ) ) ;
#19073=LINE ( 'NONE', #41367, #11580 ) ;
#19093=CIRCLE ( 'NONE', #30856, 11.59999999999999787 ) ;
#19119=CIRCLE ( 'NONE', #37887, 12.49999999999999645 ) ;
#19202=DIRECTION ( 'NONE',  ( -1.000000000000000000, 0.000000000000000000, 0.000000000000000000 ) ) ;
#19230=ORIENTED_EDGE ( 'NONE', *, *, #24921, .F. ) ;
#19292=DIRECTION ( 'NONE',  ( 0.000000000000000000, 0.000000000000000000, 1.000000000000000000 ) ) ;
#19348=AXIS2_PLACEMENT_3D ( 'NONE', #27280, #6146, #38286 ) ;
#19352=EDGE_LOOP ( 'NONE', ( #20579, #28157, #39360, #32998 ) ) ;
#19355=CARTESIAN_POINT ( 'NONE',  ( -11.59999999999999787, 0.000000000000000000, -56.19999999999998863 ) ) ;
#19403=EDGE_LOOP ( 'NONE', ( #19691, #16656, #45886, #316, #16836, #41464 ) ) ;
#19441=VERTEX_POINT ( 'NONE', #15818 ) ;
#19444=CARTESIAN_POINT ( 'NONE',  ( 6.782329983125267248, 10.49999999999999645, -125.0000000000000000 ) ) ;
#19544=EDGE_CURVE ( 'NONE', #42999, #39357, #29016, .T. ) ;
#19559=DIRECTION ( 'NONE',  ( 0.7533909544171996098, 0.6575728627325955200, -7.625282249115660656E-32 ) ) ;
#19563=VERTEX_POINT ( 'NONE', #5772 ) ;
#19610=VERTEX_POINT ( 'NONE', #25077 ) ;
#19619=ORIENTED_EDGE ( 'NONE', *, *, #42046, .T. ) ;
#19682=CARTESIAN_POINT ( 'NONE',  ( -11.59999999999999787, 0.000000000000000000, 53.20000000000001705 ) ) ;
#19691=ORIENTED_EDGE ( 'NONE', *, *, #7995, .T. ) ;
#19696=EDGE_CURVE ( 'NONE', #2616, #14712, #24844, .T. ) ;
#19742=CARTESIAN_POINT ( 'NONE',  ( -12.49999999999999645, 0.000000000000000000, 52.00000000000002132 ) ) ;
#19750=ORIENTED_EDGE ( 'NONE', *, *, #15015, .T. ) ;
#19818=FACE_OUTER_BOUND ( 'NONE', #156, .T. ) ;
#19860=CARTESIAN_POINT ( 'NONE',  ( 12.49999999999999645, 1.530808498934191127E-15, 125.0000000000000000 ) ) ;
#19939=CIRCLE ( 'NONE', #11375, 11.59999999999999787 ) ;
#19942=EDGE_CURVE ( 'NONE', #4524, #21044, #41399, .T. ) ;
#19956=PLANE ( 'NONE',  #12807 ) ;
#19957=LINE ( 'NONE', #8691, #46947 ) ;
#19960=ORIENTED_EDGE ( 'NONE', *, *, #25661, .F. ) ;
#19961=CARTESIAN_POINT ( 'NONE',  ( 0.000000000000000000, 0.000000000000000000, -43.79999999999998295 ) ) ;
#19993=EDGE_CURVE ( 'NONE', #31364, #26622, #38355, .T. ) ;
#19995=CIRCLE ( 'NONE', #1249, 11.59999999999999787 ) ;
#20018=CARTESIAN_POINT ( 'NONE',  ( 12.49999999999999645, 1.530808498934191127E-15, -54.99999999999998579 ) ) ;
#20062=ORIENTED_EDGE ( 'NONE', *, *, #16425, .T. ) ;
#20078=DIRECTION ( 'NONE',  ( -0.7533909544171996098, -0.6575728627325955200, 7.625282249115660656E-32 ) ) ;
#20136=CARTESIAN_POINT ( 'NONE',  ( 0.000000000000000000, 0.000000000000000000, 52.00000000000002132 ) ) ;
#20163=EDGE_CURVE ( 'NONE', #2616, #20736, #30875, .T. ) ;
#20172=VECTOR ( 'NONE', #15096, 1000.000000000000000 ) ;
#20263=DIRECTION ( 'NONE',  ( 1.000000000000000000, 0.000000000000000000, 0.000000000000000000 ) ) ;
#20314=ORIENTED_EDGE ( 'NONE', *, *, #19544, .F. ) ;
#20342=CARTESIAN_POINT ( 'NONE',  ( 0.000000000000000000, 0.000000000000000000, -44.99999999999998579 ) ) ;
#20358=ORIENTED_EDGE ( 'NONE', *, *, #43298, .F. ) ;
#20378=ORIENTED_EDGE ( 'NONE', *, *, #6469, .T. ) ;
#20406=ORIENTED_EDGE ( 'NONE', *, *, #18711, .T. ) ;
#20421=DIRECTION ( 'NONE',  ( -0.6575728627325955200, 0.7533909544171997208, 0.000000000000000000 ) ) ;
#20422=AXIS2_PLACEMENT_3D ( 'NONE', #45090, #31315, #4869 ) ;
#20470=ORIENTED_EDGE ( 'NONE', *, *, #19696, .T. ) ;
#20472=EDGE_CURVE ( 'NONE', #1784, #12338, #15738, .T. ) ;
#20481=CARTESIAN_POINT ( 'NONE',  ( 0.000000000000000000, 0.000000000000000000, 40.80000000000001847 ) ) ;
#20534=EDGE_LOOP ( 'NONE', ( #16035, #38492, #25539, #37460 ) ) ;
#20579=ORIENTED_EDGE ( 'NONE', *, *, #4980, .F. ) ;
#20626=DIRECTION ( 'NONE',  ( 0.000000000000000000, 0.000000000000000000, 1.000000000000000000 ) ) ;
#20684=DIRECTION ( 'NONE',  ( 0.000000000000000000, 0.000000000000000000, 1.000000000000000000 ) ) ;
#20686=DIRECTION ( 'NONE',  ( 0.7533909544171997208, 0.6575728627325956310, -6.162975822039155825E-32 ) ) ;
#20736=VERTEX_POINT ( 'NONE', #7518 ) ;
#20776=ORIENTED_EDGE ( 'NONE', *, *, #32121, .F. ) ;
#20779=ADVANCED_FACE ( 'NONE', ( #26109 ), #18269, .F. ) ;
#20798=EDGE_LOOP ( 'NONE', ( #17109, #44848, #25593, #44439 ) ) ;
#20805=ORIENTED_EDGE ( 'NONE', *, *, #46558, .F. ) ;
#20831=PRESENTATION_STYLE_ASSIGNMENT (( #6142 ) ) ;
#20840=PRODUCT_DEFINITION_CONTEXT ( 'detailed design', #9147, 'design' ) ;
#20845=EDGE_CURVE ( 'NONE', #42290, #41629, #43900, .T. ) ;
#20863=ORIENTED_EDGE ( 'NONE', *, *, #15688, .T. ) ;
#20891=CARTESIAN_POINT ( 'NONE',  ( 0.000000000000000000, 0.000000000000000000, 53.20000000000001705 ) ) ;
#20894=EDGE_CURVE ( 'NONE', #29688, #18977, #115, .T. ) ;
#20932=CARTESIAN_POINT ( 'NONE',  ( 0.000000000000000000, 0.000000000000000000, -43.79999999999998295 ) ) ;
#21015=ORIENTED_EDGE ( 'NONE', *, *, #32944, .F. ) ;
#21027=DIRECTION ( 'NONE',  ( 0.000000000000000000, 0.000000000000000000, 1.000000000000000000 ) ) ;
#21044=VERTEX_POINT ( 'NONE', #13590 ) ;
#21054=EDGE_CURVE ( 'NONE', #17275, #7609, #46406, .T. ) ;
#21086=CYLINDRICAL_SURFACE ( 'NONE', #23948, 11.59999999999999787 ) ;
#21087=CYLINDRICAL_SURFACE ( 'NONE', #39089, 11.59999999999999787 ) ;
#21103=CARTESIAN_POINT ( 'NONE',  ( 0.000000000000000000, 0.000000000000000000, -56.19999999999998863 ) ) ;
#21113=ORIENTED_EDGE ( 'NONE', *, *, #28353, .F. ) ;
#21137=AXIS2_PLACEMENT_3D ( 'NONE', #13058, #20626, #16960 ) ;
#21180=VECTOR ( 'NONE', #24230, 1000.000000000000000 ) ;
#21234=LINE ( 'NONE', #17317, #44037 ) ;
#21236=DIRECTION ( 'NONE',  ( -0.6575728627325954090, 0.7533909544171998318, 0.000000000000000000 ) ) ;
#21282=EDGE_LOOP ( 'NONE', ( #10509, #18331, #21015, #42897, #1716, #19230 ) ) ;
#21312=FACE_BOUND ( 'NONE', #631, .T. ) ;
#21330=DIRECTION ( 'NONE',  ( 0.000000000000000000, 0.000000000000000000, -1.000000000000000000 ) ) ;
#21337=ORIENTED_EDGE ( 'NONE', *, *, #32121, .T. ) ;
#21345=CARTESIAN_POINT ( 'NONE',  ( 0.000000000000000000, 0.000000000000000000, -54.99999999999998579 ) ) ;
#21347=CARTESIAN_POINT ( 'NONE',  ( 6.782329983125267248, 10.49999999999999645, -105.0000000000000000 ) ) ;
#21372=VERTEX_POINT ( 'NONE', #27510 ) ;
#21402=DIRECTION ( 'NONE',  ( 1.000000000000000000, 0.000000000000000000, 0.000000000000000000 ) ) ;
#21417=AXIS2_PLACEMENT_3D ( 'NONE', #3854, #14394, #169 ) ;
#21432=ORIENTED_EDGE ( 'NONE', *, *, #31497, .T. ) ;
#21464=DIRECTION ( 'NONE',  ( 0.000000000000000000, 0.000000000000000000, 1.000000000000000000 ) ) ;
#21493=PLANE ( 'NONE',  #44019 ) ;
#21506=ADVANCED_FACE ( 'NONE', ( #23835 ), #35321, .T. ) ;
#21552=( LENGTH_UNIT ( ) NAMED_UNIT ( * ) SI_UNIT ( .MILLI., .METRE. ) );
#21569=DIRECTION ( 'NONE',  ( 0.000000000000000000, 0.000000000000000000, 1.000000000000000000 ) ) ;
#21576=CARTESIAN_POINT ( 'NONE',  ( -11.59999999999999787, 0.000000000000000000, -43.79999999999998295 ) ) ;
#21627=VECTOR ( 'NONE', #45816, 1000.000000000000000 ) ;
#21648=ORIENTED_EDGE ( 'NONE', *, *, #20894, .T. ) ;
#21666=LINE ( 'NONE', #10892, #44851 ) ;
#21766=DIRECTION ( 'NONE',  ( 0.000000000000000000, 0.000000000000000000, 1.000000000000000000 ) ) ;
#21827=CARTESIAN_POINT ( 'NONE',  ( 11.59999999999999787, 1.420590287010929336E-15, 53.20000000000001705 ) ) ;
#21844=DIRECTION ( 'NONE',  ( 1.000000000000000000, 0.000000000000000000, 0.000000000000000000 ) ) ;
#21914=AXIS2_PLACEMENT_3D ( 'NONE', #31113, #1246, #261 ) ;
#21916=EDGE_CURVE ( 'NONE', #12855, #23067, #2873, .T. ) ;
#21934=ORIENTED_EDGE ( 'NONE', *, *, #2694, .T. ) ;
#21950=CIRCLE ( 'NONE', #16477, 11.59999999999999787 ) ;
#22017=DIRECTION ( 'NONE',  ( 0.000000000000000000, 0.000000000000000000, 1.000000000000000000 ) ) ;
#22029=ORIENTED_EDGE ( 'NONE', *, *, #7050, .T. ) ;
#22037=EDGE_CURVE ( 'NONE', #13625, #14256, #27628, .T. ) ;
#22054=DIRECTION ( 'NONE',  ( 1.000000000000000000, 0.000000000000000000, -0.000000000000000000 ) ) ;
#22064=ORIENTED_EDGE ( 'NONE', *, *, #27637, .T. ) ;
#22083=EDGE_CURVE ( 'NONE', #21044, #12855, #42466, .T. ) ;
#22107=ORIENTED_EDGE ( 'NONE', *, *, #35905, .T. ) ;
#22114=AXIS2_PLACEMENT_3D ( 'NONE', #8832, #23774, #41915 ) ;
#22153=EDGE_CURVE ( 'NONE', #46727, #22767, #15828, .T. ) ;
#22161=AXIS2_PLACEMENT_3D ( 'NONE', #15109, #11192, #44717 ) ;
#22163=CIRCLE ( 'NONE', #47938, 12.49999999999999645 ) ;
#22183=LINE ( 'NONE', #3579, #31033 ) ;
#22257=ORIENTED_EDGE ( 'NONE', *, *, #24323, .F. ) ;
#22309=LINE ( 'NONE', #3697, #26743 ) ;
#22311=CARTESIAN_POINT ( 'NONE',  ( 0.000000000000000000, 0.000000000000000000, 52.00000000000002132 ) ) ;
#22316=DIRECTION ( 'NONE',  ( 0.000000000000000000, 0.000000000000000000, 1.000000000000000000 ) ) ;
#22328=DIRECTION ( 'NONE',  ( 1.000000000000000000, 0.000000000000000000, 0.000000000000000000 ) ) ;
#22360=CLOSED_SHELL ( 'NONE', ( #23645, #11596, #37738, #31454, #10670, #26991, #18441, #2465, #44591, #21506, #43995, #20779, #40353, #42202, #12714, #27341, #14211, #30461, #16039, #39766, #25685, #3059, #47370, #27888, #42984, #33833, #4227, #15118, #15313, #32286, #14041, #2595, #44028, #9911, #44986, #46206, #38766, #15790, #42615, #2000, #12717, #28891 ) ) ;
#22393=FACE_OUTER_BOUND ( 'NONE', #16854, .T. ) ;
#22415=AXIS2_PLACEMENT_3D ( 'NONE', #18471, #11853, #40998 ) ;
#22450=CARTESIAN_POINT ( 'NONE',  ( 0.000000000000000000, 0.000000000000000000, -125.0000000000000000 ) ) ;
#22456=PLANE ( 'NONE',  #29843 ) ;
#22490=EDGE_CURVE ( 'NONE', #16462, #46727, #21666, .T. ) ;
#22535=VECTOR ( 'NONE', #33350, 1000.000000000000000 ) ;
#22580=LINE ( 'NONE', #3987, #11959 ) ;
#22590=DIRECTION ( 'NONE',  ( 8.090853898039833646E-17, -9.269810975720164453E-17, 1.000000000000000000 ) ) ;
#22594=ORIENTED_EDGE ( 'NONE', *, *, #4983, .F. ) ;
#22649=ORIENTED_EDGE ( 'NONE', *, *, #43885, .F. ) ;
#22737=LINE ( 'NONE', #15412, #44073 ) ;
#22749=UNCERTAINTY_MEASURE_WITH_UNIT (LENGTH_MEASURE( 1.000000000000000082E-05 ), #5662, 'distance_accuracy_value', 'NONE');
#22760=CIRCLE ( 'NONE', #43871, 11.59999999999999787 ) ;
#22767=VERTEX_POINT ( 'NONE', #46350 ) ;
#22800=AXIS2_PLACEMENT_3D ( 'NONE', #22450, #37368, #33924 ) ;
#22833=DIRECTION ( 'NONE',  ( -0.000000000000000000, -0.000000000000000000, -1.000000000000000000 ) ) ;
#23037=DIRECTION ( 'NONE',  ( 0.000000000000000000, 0.000000000000000000, 1.000000000000000000 ) ) ;
#23067=VERTEX_POINT ( 'NONE', #26730 ) ;
#23109=FACE_BOUND ( 'NONE', #26708, .T. ) ;
#23221=DIRECTION ( 'NONE',  ( -0.000000000000000000, -0.000000000000000000, -1.000000000000000000 ) ) ;
#23244=UNCERTAINTY_MEASURE_WITH_UNIT (LENGTH_MEASURE( 1.000000000000000082E-05 ), #33518, 'distance_accuracy_value', 'NONE');
#23262=CIRCLE ( 'NONE', #37315, 12.49999999999999645 ) ;
#23274=VECTOR ( 'NONE', #22017, 1000.000000000000000 ) ;
#23325=DIRECTION ( 'NONE',  ( 0.000000000000000000, 0.000000000000000000, 1.000000000000000000 ) ) ;
#23351=FACE_OUTER_BOUND ( 'NONE', #9812, .T. ) ;
#23391=DIRECTION ( 'NONE',  ( 0.000000000000000000, 0.000000000000000000, 1.000000000000000000 ) ) ;
#23470=DIRECTION ( 'NONE',  ( 1.000000000000000000, 0.000000000000000000, 0.000000000000000000 ) ) ;
#23590=AXIS2_PLACEMENT_3D ( 'NONE', #20136, #23325, #27249 ) ;
#23615=DIRECTION ( 'NONE',  ( 1.000000000000000000, 0.000000000000000000, 0.000000000000000000 ) ) ;
#23629=DIRECTION ( 'NONE',  ( 1.000000000000000000, 0.000000000000000000, -0.000000000000000000 ) ) ;
#23645=ADVANCED_FACE ( 'NONE', ( #24378 ), #32680, .T. ) ;
#23774=DIRECTION ( 'NONE',  ( 0.000000000000000000, 0.000000000000000000, 1.000000000000000000 ) ) ;
#23820=CIRCLE ( 'NONE', #18320, 12.49999999999999645 ) ;
#23835=FACE_OUTER_BOUND ( 'NONE', #1336, .T. ) ;
#23854=ORIENTED_EDGE ( 'NONE', *, *, #19993, .T. ) ;
#23948=AXIS2_PLACEMENT_3D ( 'NONE', #32365, #21330, #24778 ) ;
#23970=EDGE_LOOP ( 'NONE', ( #9996, #29040, #7415, #46588 ) ) ;
#24078=DIRECTION ( 'NONE',  ( -0.000000000000000000, -0.000000000000000000, -1.000000000000000000 ) ) ;
#24095=MECHANICAL_DESIGN_GEOMETRIC_PRESENTATION_REPRESENTATION('',(#17063),#17822);
#24165=ORIENTED_EDGE ( 'NONE', *, *, #32539, .T. ) ;
#24230=DIRECTION ( 'NONE',  ( 0.6575728627325957421, -0.7533909544171994987, 0.000000000000000000 ) ) ;
#24254=EDGE_CURVE ( 'NONE', #46727, #34724, #19995, .T. ) ;
#24303=DIRECTION ( 'NONE',  ( 0.000000000000000000, 0.000000000000000000, 1.000000000000000000 ) ) ;
#24323=EDGE_CURVE ( 'NONE', #8099, #46550, #7502, .T. ) ;
#24350=FACE_OUTER_BOUND ( 'NONE', #29397, .T. ) ;
#24378=FACE_OUTER_BOUND ( 'NONE', #14690, .T. ) ;
#24389=CARTESIAN_POINT ( 'NONE',  ( 0.000000000000000000, 0.000000000000000000, 125.0000000000000000 ) ) ;
#24440=DIRECTION ( 'NONE',  ( 0.000000000000000000, 0.000000000000000000, 1.000000000000000000 ) ) ;
#24461=DIRECTION ( 'NONE',  ( 1.000000000000000000, 0.000000000000000000, 0.000000000000000000 ) ) ;
#24496=( NAMED_UNIT ( * ) PLANE_ANGLE_UNIT ( ) SI_UNIT ( $, .RADIAN. ) );
#24534=DIRECTION ( 'NONE',  ( -1.000000000000000000, 0.000000000000000000, 0.000000000000000000 ) ) ;
#24539=ORIENTED_EDGE ( 'NONE', *, *, #44734, .T. ) ;
#24633=VECTOR ( 'NONE', #2806, 1000.000000000000000 ) ;
#24657=ORIENTED_EDGE ( 'NONE', *, *, #26934, .F. ) ;
#24680=CARTESIAN_POINT ( 'NONE',  ( -12.40464318976454727, 10.41032311384371845, -55.00000000000000000 ) ) ;
#24778=DIRECTION ( 'NONE',  ( -1.000000000000000000, 0.000000000000000000, 0.000000000000000000 ) ) ;
#24837=ORIENTED_EDGE ( 'NONE', *, *, #39027, .F. ) ;
#24844=LINE ( 'NONE', #32200, #14099 ) ;
#24847=CARTESIAN_POINT ( 'NONE',  ( -11.59999999999999787, 0.000000000000000000, -43.79999999999998295 ) ) ;
#24853=CARTESIAN_POINT ( 'NONE',  ( -12.49999999999999645, 0.000000000000000000, 125.0000000000000000 ) ) ;
#24915=ORIENTED_EDGE ( 'NONE', *, *, #32539, .F. ) ;
#24921=EDGE_CURVE ( 'NONE', #19610, #22767, #22183, .T. ) ;
#25077=CARTESIAN_POINT ( 'NONE',  ( -9.937067298023309903, 7.583184918921312523, 52.00000000000002132 ) ) ;
#25082=EDGE_LOOP ( 'NONE', ( #7961, #1811, #27255, #22649, #1394, #31202 ) ) ;
#25124=CARTESIAN_POINT ( 'NONE',  ( 0.000000000000000000, 0.000000000000000000, -44.99999999999998579 ) ) ;
#25125=EDGE_CURVE ( 'NONE', #40697, #36269, #38822, .T. ) ;
#25224=CIRCLE ( 'NONE', #42448, 11.59999999999999787 ) ;
#25314=CARTESIAN_POINT ( 'NONE',  ( -12.49999999999999645, 0.000000000000000000, 125.0000000000000000 ) ) ;
#25359=AXIS2_PLACEMENT_3D ( 'NONE', #28646, #40389, #10033 ) ;
#25414=AXIS2_PLACEMENT_3D ( 'NONE', #20891, #39742, #48024 ) ;
#25421=CARTESIAN_POINT ( 'NONE',  ( -7.469491406282117829, 4.756046723998917258, -64.01812422950395387 ) ) ;
#25467=EDGE_LOOP ( 'NONE', ( #9887, #20406 ) ) ;
#25518=ORIENTED_EDGE ( 'NONE', *, *, #47506, .T. ) ;
#25539=ORIENTED_EDGE ( 'NONE', *, *, #26136, .T. ) ;
#25593=ORIENTED_EDGE ( 'NONE', *, *, #14426, .T. ) ;
#25641=CARTESIAN_POINT ( 'NONE',  ( 0.000000000000000000, 0.000000000000000000, 52.00000000000002132 ) ) ;
#25661=EDGE_CURVE ( 'NONE', #31364, #40697, #25722, .T. ) ;
#25671=DIRECTION ( 'NONE',  ( -0.000000000000000000, -0.000000000000000000, -1.000000000000000000 ) ) ;
#25685=ADVANCED_FACE ( 'NONE', ( #44097, #18132 ), #7135, .F. ) ;
#25720=DIRECTION ( 'NONE',  ( 1.000000000000000000, 0.000000000000000000, 0.000000000000000000 ) ) ;
#25722=LINE ( 'NONE', #17668, #29505 ) ;
#25740=ORIENTED_EDGE ( 'NONE', *, *, #43456, .T. ) ;
#25800=DIRECTION ( 'NONE',  ( 1.000000000000000000, 0.000000000000000000, 0.000000000000000000 ) ) ;
#25821=VECTOR ( 'NONE', #12031, 1000.000000000000000 ) ;
#25860=DIRECTION ( 'NONE',  ( 1.000000000000000000, 0.000000000000000000, 0.000000000000000000 ) ) ;
#26076=AXIS2_PLACEMENT_3D ( 'NONE', #36718, #21569, #2712 ) ;
#26083=DIRECTION ( 'NONE',  ( 0.000000000000000000, 0.000000000000000000, 1.000000000000000000 ) ) ;
#26088=ORIENTED_EDGE ( 'NONE', *, *, #16460, .F. ) ;
#26108=ORIENTED_EDGE ( 'NONE', *, *, #10987, .F. ) ;
#26109=FACE_OUTER_BOUND ( 'NONE', #46409, .T. ) ;
#26136=EDGE_CURVE ( 'NONE', #13625, #12338, #33450, .T. ) ;
#26313=CYLINDRICAL_SURFACE ( 'NONE', #26925, 12.49999999999999645 ) ;
#26370=AXIS2_PLACEMENT_3D ( 'NONE', #10656, #3048, #39793 ) ;
#26557=VERTEX_POINT ( 'NONE', #40992 ) ;
#26622=VERTEX_POINT ( 'NONE', #3277 ) ;
#26708=EDGE_LOOP ( 'NONE', ( #24837, #43028 ) ) ;
#26730=CARTESIAN_POINT ( 'NONE',  ( -9.937067298023317008, 7.583184918921301865, -54.99999999999999289 ) ) ;
#26743=VECTOR ( 'NONE', #33552, 1000.000000000000000 ) ;
#26909=VECTOR ( 'NONE', #22833, 1000.000000000000000 ) ;
#26925=AXIS2_PLACEMENT_3D ( 'NONE', #18942, #4291, #19202 ) ;
#26934=EDGE_CURVE ( 'NONE', #36269, #40640, #44588, .T. ) ;
#26952=CARTESIAN_POINT ( 'NONE',  ( 0.000000000000000000, 0.000000000000000000, -54.99999999999998579 ) ) ;
#26987=EDGE_CURVE ( 'NONE', #32749, #16632, #48015, .T. ) ;
#26991=ADVANCED_FACE ( 'NONE', ( #14504 ), #28928, .T. ) ;
#27017=ORIENTED_EDGE ( 'NONE', *, *, #5747, .F. ) ;
#27067=ORIENTED_EDGE ( 'NONE', *, *, #25125, .F. ) ;
#27143=CIRCLE ( 'NONE', #22415, 12.49999999999999645 ) ;
#27153=EDGE_LOOP ( 'NONE', ( #649, #26088, #38864, #19619 ) ) ;
#27247=CARTESIAN_POINT ( 'NONE',  ( 11.59999999999999787, 1.420590287010929336E-15, -54.99999999999998579 ) ) ;
#27249=DIRECTION ( 'NONE',  ( 1.000000000000000000, 0.000000000000000000, -0.000000000000000000 ) ) ;
#27255=ORIENTED_EDGE ( 'NONE', *, *, #14053, .T. ) ;
#27280=CARTESIAN_POINT ( 'NONE',  ( 0.000000000000000000, 0.000000000000000000, 125.0000000000000000 ) ) ;
#27341=ADVANCED_FACE ( 'NONE', ( #47954 ), #33277, .F. ) ;
#27348=AXIS2_PLACEMENT_3D ( 'NONE', #19961, #23391, #31738 ) ;
#27451=AXIS2_PLACEMENT_3D ( 'NONE', #20481, #1416, #16827 ) ;
#27453=DIRECTION ( 'NONE',  ( 1.000000000000000000, 0.000000000000000000, 0.000000000000000000 ) ) ;
#27455=VECTOR ( 'NONE', #20078, 1000.000000000000114 ) ;
#27510=CARTESIAN_POINT ( 'NONE',  ( -6.782329983125267248, 10.49999999999999645, -104.9999999999999858 ) ) ;
#27542=CARTESIAN_POINT ( 'NONE',  ( -8.637688417678527131, 13.69818742750669394, 52.00000000000002132 ) ) ;
#27562=DIRECTION ( 'NONE',  ( 1.000000000000000000, 0.000000000000000000, 0.000000000000000000 ) ) ;
#27589=ORIENTED_EDGE ( 'NONE', *, *, #18711, .F. ) ;
#27597=CARTESIAN_POINT ( 'NONE',  ( 11.59999999999999787, 1.420590287010929336E-15, 53.20000000000001705 ) ) ;
#27628=CIRCLE ( 'NONE', #22161, 12.49999999999999645 ) ;
#27637=EDGE_CURVE ( 'NONE', #32290, #26557, #6524, .T. ) ;
#27638=CIRCLE ( 'NONE', #7282, 11.59999999999999787 ) ;
#27792=CARTESIAN_POINT ( 'NONE',  ( 0.000000000000000000, 0.000000000000000000, 125.0000000000000000 ) ) ;
#27808=CYLINDRICAL_SURFACE ( 'NONE', #357, 12.49999999999999645 ) ;
#27843=VERTEX_POINT ( 'NONE', #19682 ) ;
#27847=ORIENTED_EDGE ( 'NONE', *, *, #40960, .F. ) ;
#27853=LINE ( 'NONE', #34674, #13260 ) ;
#27888=ADVANCED_FACE ( 'NONE', ( #8928 ), #5502, .T. ) ;
#27954=FILL_AREA_STYLE ('',( #36229 ) ) ;
#27983=ORIENTED_EDGE ( 'NONE', *, *, #27637, .F. ) ;
#28044=CARTESIAN_POINT ( 'NONE',  ( 11.59999999999999787, 1.420590287010929336E-15, -44.99999999999998579 ) ) ;
#28080=ORIENTED_EDGE ( 'NONE', *, *, #29900, .T. ) ;
#28114=AXIS2_PLACEMENT_3D ( 'NONE', #24389, #39328, #5810 ) ;
#28138=DIRECTION ( 'NONE',  ( 0.000000000000000000, 0.000000000000000000, 1.000000000000000000 ) ) ;
#28157=ORIENTED_EDGE ( 'NONE', *, *, #48050, .F. ) ;
#28180=DIRECTION ( 'NONE',  ( 0.000000000000000000, 0.000000000000000000, -1.000000000000000000 ) ) ;
#28192=CARTESIAN_POINT ( 'NONE',  ( 0.000000000000000000, 0.000000000000000000, -54.99999999999998579 ) ) ;
#28284=AXIS2_PLACEMENT_3D ( 'NONE', #18025, #32963, #47886 ) ;
#28311=EDGE_LOOP ( 'NONE', ( #5784, #5091, #47627, #36628 ) ) ;
#28350=CARTESIAN_POINT ( 'NONE',  ( -8.637688417678527131, 13.69818742750669394, 32.98187577049606745 ) ) ;
#28353=EDGE_CURVE ( 'NONE', #34027, #1594, #36823, .T. ) ;
#28464=DIRECTION ( 'NONE',  ( 1.000000000000000000, 0.000000000000000000, 0.000000000000000000 ) ) ;
#28524=EDGE_CURVE ( 'NONE', #8199, #46824, #44355, .T. ) ;
#28551=ORIENTED_EDGE ( 'NONE', *, *, #22490, .F. ) ;
#28646=CARTESIAN_POINT ( 'NONE',  ( -1.734723475976807094E-14, 1.040834085586084257E-14, -45.00000000000000000 ) ) ;
#28739=EDGE_LOOP ( 'NONE', ( #46930, #37967, #3865, #45006 ) ) ;
#28759=DIRECTION ( 'NONE',  ( 0.000000000000000000, 0.000000000000000000, 1.000000000000000000 ) ) ;
#28839=CARTESIAN_POINT ( 'NONE',  ( -5.565113727472255967, 10.17789316117534248, -44.99999999999998579 ) ) ;
#28882=( NAMED_UNIT ( * ) SI_UNIT ( $, .STERADIAN. ) SOLID_ANGLE_UNIT ( ) );
#28891=ADVANCED_FACE ( 'NONE', ( #8239 ), #22456, .F. ) ;
#28907=CARTESIAN_POINT ( 'NONE',  ( -9.937067298023317008, 7.583184918921300977, -44.99999999999998579 ) ) ;
#28928=CYLINDRICAL_SURFACE ( 'NONE', #44515, 12.49999999999999645 ) ;
#28931=ORIENTED_EDGE ( 'NONE', *, *, #47712, .F. ) ;
#28945=LINE ( 'NONE', #3489, #22535 ) ;
#28975=DIRECTION ( 'NONE',  ( -0.000000000000000000, -0.000000000000000000, -1.000000000000000000 ) ) ;
#28982=FACE_BOUND ( 'NONE', #31699, .T. ) ;
#29016=CIRCLE ( 'NONE', #27348, 12.49999999999999645 ) ;
#29040=ORIENTED_EDGE ( 'NONE', *, *, #42371, .F. ) ;
#29049=CARTESIAN_POINT ( 'NONE',  ( 0.000000000000000000, 0.000000000000000000, -54.99999999999998579 ) ) ;
#29053=ORIENTED_EDGE ( 'NONE', *, *, #3696, .T. ) ;
#29094=DIRECTION ( 'NONE',  ( 0.7533909544171998318, 0.6575728627325954090, 0.000000000000000000 ) ) ;
#29189=CARTESIAN_POINT ( 'NONE',  ( 0.000000000000000000, 0.000000000000000000, -54.99999999999998579 ) ) ;
#29216=DIRECTION ( 'NONE',  ( 1.000000000000000000, 0.000000000000000000, 0.000000000000000000 ) ) ;
#29337=ORIENTED_EDGE ( 'NONE', *, *, #15897, .F. ) ;
#29345=EDGE_LOOP ( 'NONE', ( #43893, #15, #6755, #2296 ) ) ;
#29362=ORIENTED_EDGE ( 'NONE', *, *, #15015, .F. ) ;
#29397=EDGE_LOOP ( 'NONE', ( #9715, #22257, #48122, #48000 ) ) ;
#29417=CARTESIAN_POINT ( 'NONE',  ( -8.637688417678548447, 13.69818742750669749, -55.00000000000000000 ) ) ;
#29505=VECTOR ( 'NONE', #6664, 1000.000000000000000 ) ;
#29518=CARTESIAN_POINT ( 'NONE',  ( -7.469491406282094736, 4.756046723998911929, 42.00000000000001421 ) ) ;
#29600=DIRECTION ( 'NONE',  ( 0.7533909544171998318, 0.6575728627325954090, 0.000000000000000000 ) ) ;
#29602=CARTESIAN_POINT ( 'NONE',  ( -12.40464318976454905, 10.41032311384371845, -64.01812422950393966 ) ) ;
#29635=CARTESIAN_POINT ( 'NONE',  ( -12.49999999999999645, 0.000000000000000000, 42.00000000000001421 ) ) ;
#29656=CARTESIAN_POINT ( 'NONE',  ( 0.000000000000000000, 0.000000000000000000, -44.99999999999998579 ) ) ;
#29688=VERTEX_POINT ( 'NONE', #15475 ) ;
#29753=ORIENTED_EDGE ( 'NONE', *, *, #34973, .T. ) ;
#29783=CARTESIAN_POINT ( 'NONE',  ( 0.000000000000000000, 0.000000000000000000, -105.0000000000000000 ) ) ;
#29843=AXIS2_PLACEMENT_3D ( 'NONE', #29783, #30286, #37377 ) ;
#29900=EDGE_CURVE ( 'NONE', #31057, #2616, #11195, .T. ) ;
#29963=AXIS2_PLACEMENT_3D ( 'NONE', #31939, #39994, #43430 ) ;
#29977=FACE_OUTER_BOUND ( 'NONE', #28739, .T. ) ;
#30071=AXIS2_PLACEMENT_3D ( 'NONE', #18001, #26083, #3566 ) ;
#30181=CARTESIAN_POINT ( 'NONE',  ( 12.49999999999999645, 1.530808498934191127E-15, 42.00000000000001421 ) ) ;
#30285=DIRECTION ( 'NONE',  ( 0.000000000000000000, 0.000000000000000000, 1.000000000000000000 ) ) ;
#30286=DIRECTION ( 'NONE',  ( 0.000000000000000000, -0.000000000000000000, 1.000000000000000000 ) ) ;
#30333=DIRECTION ( 'NONE',  ( -1.000000000000000000, 0.000000000000000000, 0.000000000000000000 ) ) ;
#30395=EDGE_CURVE ( 'NONE', #15125, #16632, #4212, .T. ) ;
#30461=ADVANCED_FACE ( 'NONE', ( #43050 ), #21493, .F. ) ;
#30466=PLANE ( 'NONE',  #30838 ) ;
#30474=ORIENTED_EDGE ( 'NONE', *, *, #39145, .F. ) ;
#30554=EDGE_CURVE ( 'NONE', #17275, #45171, #44865, .T. ) ;
#30564=ORIENTED_EDGE ( 'NONE', *, *, #5747, .T. ) ;
#30671=DIRECTION ( 'NONE',  ( -0.000000000000000000, -0.000000000000000000, -1.000000000000000000 ) ) ;
#30698=AXIS2_PLACEMENT_3D ( 'NONE', #3159, #24078, #43407 ) ;
#30838=AXIS2_PLACEMENT_3D ( 'NONE', #45381, #39252, #5982 ) ;
#30843=ORIENTED_EDGE ( 'NONE', *, *, #42371, .T. ) ;
#30856=AXIS2_PLACEMENT_3D ( 'NONE', #16154, #5134, #23470 ) ;
#30875=LINE ( 'NONE', #1248, #25821 ) ;
#30889=CARTESIAN_POINT ( 'NONE',  ( 12.49999999999999645, 1.530808498934191127E-15, 125.0000000000000000 ) ) ;
#30902=AXIS2_PLACEMENT_3D ( 'NONE', #18623, #14479, #33551 ) ;
#30907=ORIENTED_EDGE ( 'NONE', *, *, #10186, .F. ) ;
#30934=CARTESIAN_POINT ( 'NONE',  ( -12.49999999999999645, 0.000000000000000000, -44.99999999999998579 ) ) ;
#31033=VECTOR ( 'NONE', #18513, 1000.000000000000000 ) ;
#31057=VERTEX_POINT ( 'NONE', #30181 ) ;
#31067=EDGE_CURVE ( 'NONE', #34023, #12855, #22580, .T. ) ;
#31113=CARTESIAN_POINT ( 'NONE',  ( 0.000000000000000000, 0.000000000000000000, 53.20000000000001705 ) ) ;
#31171=CARTESIAN_POINT ( 'NONE',  ( 12.49999999999999645, 1.530808498934191127E-15, 125.0000000000000000 ) ) ;
#31173=EDGE_LOOP ( 'NONE', ( #39804, #43670, #20062, #22107, #34602, #34044 ) ) ;
#31191=FACE_OUTER_BOUND ( 'NONE', #33252, .T. ) ;
#31202=ORIENTED_EDGE ( 'NONE', *, *, #2653, .F. ) ;
#31223=CARTESIAN_POINT ( 'NONE',  ( 0.000000000000000000, 0.000000000000000000, -54.99999999999998579 ) ) ;
#31249=DIRECTION ( 'NONE',  ( -0.000000000000000000, -0.000000000000000000, -1.000000000000000000 ) ) ;
#31267=EDGE_LOOP ( 'NONE', ( #4612, #40630 ) ) ;
#31287=ORIENTED_EDGE ( 'NONE', *, *, #31332, .F. ) ;
#31315=DIRECTION ( 'NONE',  ( 0.000000000000000000, 0.000000000000000000, 1.000000000000000000 ) ) ;
#31332=EDGE_CURVE ( 'NONE', #19563, #16462, #10054, .T. ) ;
#31335=CIRCLE ( 'NONE', #21137, 11.59999999999999787 ) ;
#31345=VECTOR ( 'NONE', #37716, 1000.000000000000114 ) ;
#31364=VERTEX_POINT ( 'NONE', #10785 ) ;
#31389=CIRCLE ( 'NONE', #10247, 12.49999999999999645 ) ;
#31454=ADVANCED_FACE ( 'NONE', ( #40631 ), #18360, .T. ) ;
#31497=EDGE_CURVE ( 'NONE', #40640, #31364, #19093, .T. ) ;
#31576=AXIS2_PLACEMENT_3D ( 'NONE', #6329, #24440, #5857 ) ;
#31638=LINE ( 'NONE', #35042, #33113 ) ;
#31663=CIRCLE ( 'NONE', #30071, 11.59999999999999787 ) ;
#31695=ORIENTED_EDGE ( 'NONE', *, *, #29900, .F. ) ;
#31699=EDGE_LOOP ( 'NONE', ( #5409, #11955 ) ) ;
#31738=DIRECTION ( 'NONE',  ( 1.000000000000000000, 0.000000000000000000, 0.000000000000000000 ) ) ;
#31815=CARTESIAN_POINT ( 'NONE',  ( 12.49999999999999645, 1.530808498934191127E-15, 52.00000000000002132 ) ) ;
#31852=ORIENTED_EDGE ( 'NONE', *, *, #4980, .T. ) ;
#31903=EDGE_CURVE ( 'NONE', #8099, #17326, #17492, .T. ) ;
#31923=DIRECTION ( 'NONE',  ( 0.000000000000000000, 0.000000000000000000, 1.000000000000000000 ) ) ;
#31939=CARTESIAN_POINT ( 'NONE',  ( 0.000000000000000000, 0.000000000000000000, -44.99999999999998579 ) ) ;
#31956=DIRECTION ( 'NONE',  ( 0.000000000000000000, 0.000000000000000000, 1.000000000000000000 ) ) ;
#32121=EDGE_CURVE ( 'NONE', #21044, #32290, #15563, .T. ) ;
#32122=PLANE ( 'NONE',  #39117 ) ;
#32148=VECTOR ( 'NONE', #5176, 1000.000000000000114 ) ;
#32163=DIRECTION ( 'NONE',  ( 0.000000000000000000, 0.000000000000000000, -1.000000000000000000 ) ) ;
#32200=CARTESIAN_POINT ( 'NONE',  ( -8.637688417678527131, 13.69818742750669394, 42.00000000000001421 ) ) ;
#32286=ADVANCED_FACE ( 'NONE', ( #36570, #28982 ), #39549, .F. ) ;
#32290=VERTEX_POINT ( 'NONE', #10145 ) ;
#32365=CARTESIAN_POINT ( 'NONE',  ( 0.000000000000000000, 0.000000000000000000, 42.00000000000001421 ) ) ;
#32428=CARTESIAN_POINT ( 'NONE',  ( 12.49999999999999645, 1.530808498934191127E-15, 125.0000000000000000 ) ) ;
#32435=CARTESIAN_POINT ( 'NONE',  ( -11.59999999999999787, 0.000000000000000000, -54.99999999999998579 ) ) ;
#32536=CARTESIAN_POINT ( 'NONE',  ( 0.000000000000000000, 0.000000000000000000, 42.00000000000001421 ) ) ;
#32539=EDGE_CURVE ( 'NONE', #46550, #20736, #41902, .T. ) ;
#32568=SURFACE_SIDE_STYLE ('',( #35517 ) ) ;
#32600=DIRECTION ( 'NONE',  ( 0.000000000000000000, 0.000000000000000000, 1.000000000000000000 ) ) ;
#32609=ORIENTED_EDGE ( 'NONE', *, *, #21916, .F. ) ;
#32680=CYLINDRICAL_SURFACE ( 'NONE', #38721, 12.49999999999999645 ) ;
#32749=VERTEX_POINT ( 'NONE', #38997 ) ;
#32944=EDGE_CURVE ( 'NONE', #16462, #40697, #751, .T. ) ;
#32957=CYLINDRICAL_SURFACE ( 'NONE', #5675, 11.59999999999999787 ) ;
#32963=DIRECTION ( 'NONE',  ( 0.000000000000000000, 0.000000000000000000, 1.000000000000000000 ) ) ;
#32998=ORIENTED_EDGE ( 'NONE', *, *, #7083, .T. ) ;
#33034=FILL_AREA_STYLE_COLOUR ( '', #1472 ) ;
#33113=VECTOR ( 'NONE', #28180, 1000.000000000000000 ) ;
#33188=DIRECTION ( 'NONE',  ( 0.000000000000000000, 0.000000000000000000, 1.000000000000000000 ) ) ;
#33227=LINE ( 'NONE', #37137, #43594 ) ;
#33252=EDGE_LOOP ( 'NONE', ( #47342, #21648 ) ) ;
#33277=PLANE ( 'NONE',  #5468 ) ;
#33333=CARTESIAN_POINT ( 'NONE',  ( 0.000000000000000000, 0.000000000000000000, 53.20000000000001705 ) ) ;
#33350=DIRECTION ( 'NONE',  ( 0.6575728627325955200, -0.7533909544171997208, 0.000000000000000000 ) ) ;
#33440=ORIENTED_EDGE ( 'NONE', *, *, #4538, .F. ) ;
#33450=LINE ( 'NONE', #148, #20172 ) ;
#33457=ORIENTED_EDGE ( 'NONE', *, *, #4690, .F. ) ;
#33479=COLOUR_RGB ( '', 0.72549020, 0.75294118, 0.79215686) ;
#33515=CIRCLE ( 'NONE', #35096, 11.59999999999999787 ) ;
#33518=( LENGTH_UNIT ( ) NAMED_UNIT ( * ) SI_UNIT ( .MILLI., .METRE. ) );
#33532=MECHANICAL_DESIGN_GEOMETRIC_PRESENTATION_REPRESENTATION('',(#42921),#35881);
#33551=DIRECTION ( 'NONE',  ( 1.000000000000000000, 0.000000000000000000, 0.000000000000000000 ) ) ;
#33552=DIRECTION ( 'NONE',  ( -0.000000000000000000, -0.000000000000000000, -1.000000000000000000 ) ) ;
#33595=FACE_OUTER_BOUND ( 'NONE', #21282, .T. ) ;
#33601=FACE_OUTER_BOUND ( 'NONE', #11526, .T. ) ;
#33626=CIRCLE ( 'NONE', #17305, 11.59999999999999787 ) ;
#33669=ORIENTED_EDGE ( 'NONE', *, *, #22153, .F. ) ;
#33756=VECTOR ( 'NONE', #13120, 1000.000000000000000 ) ;
#33775=ORIENTED_EDGE ( 'NONE', *, *, #42232, .T. ) ;
#33833=ADVANCED_FACE ( 'NONE', ( #31191, #23109 ), #38521, .T. ) ;
#33864=AXIS2_PLACEMENT_3D ( 'NONE', #48150, #40806, #47894 ) ;
#33904=AXIS2_PLACEMENT_3D ( 'NONE', #63, #22590, #15265 ) ;
#33924=DIRECTION ( 'NONE',  ( 1.000000000000000000, 0.000000000000000000, -0.000000000000000000 ) ) ;
#33957=VECTOR ( 'NONE', #41977, 1000.000000000000000 ) ;
#33965=ORIENTED_EDGE ( 'NONE', *, *, #47712, .T. ) ;
#33978=CARTESIAN_POINT ( 'NONE',  ( 0.000000000000000000, 0.000000000000000000, 42.00000000000001421 ) ) ;
#34023=VERTEX_POINT ( 'NONE', #10101 ) ;
#34027=VERTEX_POINT ( 'NONE', #36524 ) ;
#34044=ORIENTED_EDGE ( 'NONE', *, *, #21054, .F. ) ;
#34086=CIRCLE ( 'NONE', #30902, 12.49999999999999645 ) ;
#34217=DIRECTION ( 'NONE',  ( 1.000000000000000000, 0.000000000000000000, 0.000000000000000000 ) ) ;
#34301=EDGE_CURVE ( 'NONE', #16579, #15125, #42626, .T. ) ;
#34402=CARTESIAN_POINT ( 'NONE',  ( -12.40464318976452596, 10.41032311384371489, 42.00000000000001421 ) ) ;
#34460=FACE_OUTER_BOUND ( 'NONE', #5568, .T. ) ;
#34487=AXIS2_PLACEMENT_3D ( 'NONE', #42553, #15627, #20263 ) ;
#34505=CARTESIAN_POINT ( 'NONE',  ( -6.170112525937322623, 10.87104923258428180, -54.99999999999998579 ) ) ;
#34602=ORIENTED_EDGE ( 'NONE', *, *, #14385, .T. ) ;
#34665=ORIENTED_EDGE ( 'NONE', *, *, #8655, .F. ) ;
#34674=CARTESIAN_POINT ( 'NONE',  ( 11.59999999999999787, 1.420590287010929336E-15, -43.79999999999998295 ) ) ;
#34709=CYLINDRICAL_SURFACE ( 'NONE', #18151, 12.49999999999999645 ) ;
#34724=VERTEX_POINT ( 'NONE', #16372 ) ;
#34891=DIRECTION ( 'NONE',  ( 0.000000000000000000, 0.000000000000000000, -1.000000000000000000 ) ) ;
#34908=LINE ( 'NONE', #24853, #47444 ) ;
#34920=ORIENTED_EDGE ( 'NONE', *, *, #10743, .T. ) ;
#34973=EDGE_CURVE ( 'NONE', #21372, #46304, #33227, .T. ) ;
#34991=ORIENTED_EDGE ( 'NONE', *, *, #28353, .T. ) ;
#35042=CARTESIAN_POINT ( 'NONE',  ( -11.59999999999999787, 0.000000000000000000, 53.20000000000001705 ) ) ;
#35096=AXIS2_PLACEMENT_3D ( 'NONE', #25124, #21464, #3088 ) ;
#35097=DIRECTION ( 'NONE',  ( 0.000000000000000000, 0.000000000000000000, 1.000000000000000000 ) ) ;
#35100=FACE_OUTER_BOUND ( 'NONE', #35499, .T. ) ;
#35149=ORIENTED_EDGE ( 'NONE', *, *, #43456, .F. ) ;
#35191=ORIENTED_EDGE ( 'NONE', *, *, #31332, .T. ) ;
#35234=EDGE_LOOP ( 'NONE', ( #14888, #42151, #18115, #34920 ) ) ;
#35306=ORIENTED_EDGE ( 'NONE', *, *, #15688, .F. ) ;
#35321=CYLINDRICAL_SURFACE ( 'NONE', #30698, 12.49999999999999645 ) ;
#35371=DIRECTION ( 'NONE',  ( 0.000000000000000000, 0.000000000000000000, 1.000000000000000000 ) ) ;
#35499=EDGE_LOOP ( 'NONE', ( #42321, #30474, #29053, #20863 ) ) ;
#35512=CIRCLE ( 'NONE', #6576, 12.49999999999999645 ) ;
#35517=SURFACE_STYLE_FILL_AREA ( #27954 ) ;
#35626=MANIFOLD_SOLID_BREP ( 'Cut-Extrude1', #22360 ) ;
#35762=ORIENTED_EDGE ( 'NONE', *, *, #15039, .F. ) ;
#35881=( GEOMETRIC_REPRESENTATION_CONTEXT ( 3 ) GLOBAL_UNCERTAINTY_ASSIGNED_CONTEXT ( ( #23244 ) ) GLOBAL_UNIT_ASSIGNED_CONTEXT ( ( #33518, #48447, #28882 ) ) REPRESENTATION_CONTEXT ( 'NONE', 'WORKASPACE' ) );
#35905=EDGE_CURVE ( 'NONE', #15072, #15224, #33515, .T. ) ;
#36169=CIRCLE ( 'NONE', #207, 11.59999999999999787 ) ;
#36187=ORIENTED_EDGE ( 'NONE', *, *, #10984, .F. ) ;
#36188=ORIENTED_EDGE ( 'NONE', *, *, #12074, .F. ) ;
#36202=LINE ( 'NONE', #25421, #40054 ) ;
#36229=FILL_AREA_STYLE_COLOUR ( '', #33479 ) ;
#36230=( NAMED_UNIT ( * ) PLANE_ANGLE_UNIT ( ) SI_UNIT ( $, .RADIAN. ) );
#36269=VERTEX_POINT ( 'NONE', #19022 ) ;
#36283=PRODUCT ( 'Input Shaft', 'Input Shaft', '', ( #38737 ) ) ;
#36285=DIRECTION ( 'NONE',  ( -0.000000000000000000, -0.000000000000000000, -1.000000000000000000 ) ) ;
#36348=PLANE ( 'NONE',  #26370 ) ;
#36376=ORIENTED_EDGE ( 'NONE', *, *, #47506, .F. ) ;
#36450=VERTEX_POINT ( 'NONE', #1407 ) ;
#36465=CARTESIAN_POINT ( 'NONE',  ( 5.377855484467702900E-15, 4.693886760319831848E-15, 52.00000000000002132 ) ) ;
#36524=CARTESIAN_POINT ( 'NONE',  ( 11.59999999999999787, 1.420590287010929336E-15, -56.19999999999998863 ) ) ;
#36570=FACE_OUTER_BOUND ( 'NONE', #47054, .T. ) ;
#36628=ORIENTED_EDGE ( 'NONE', *, *, #8655, .T. ) ;
#36631=DIRECTION ( 'NONE',  ( -1.000000000000000000, 0.000000000000000000, 0.000000000000000000 ) ) ;
#36632=CIRCLE ( 'NONE', #10048, 12.49999999999999645 ) ;
#36659=DIRECTION ( 'NONE',  ( 0.000000000000000000, 0.000000000000000000, 1.000000000000000000 ) ) ;
#36718=CARTESIAN_POINT ( 'NONE',  ( 0.000000000000000000, 0.000000000000000000, -56.19999999999998863 ) ) ;
#36751=CARTESIAN_POINT ( 'NONE',  ( 0.000000000000000000, 0.000000000000000000, 125.0000000000000000 ) ) ;
#36823=CIRCLE ( 'NONE', #7894, 11.59999999999999787 ) ;
#36846=DIRECTION ( 'NONE',  ( 1.000000000000000000, 0.000000000000000000, 0.000000000000000000 ) ) ;
#36863=DIRECTION ( 'NONE',  ( 0.6575728627325955200, -0.7533909544171996098, -1.230411769795008318E-16 ) ) ;
#36967=CARTESIAN_POINT ( 'NONE',  ( -5.565113727472242644, 10.17789316117535137, 52.00000000000002132 ) ) ;
#36995=CARTESIAN_POINT ( 'NONE',  ( -8.637688417678527131, 13.69818742750669394, 52.00000000000002132 ) ) ;
#37137=CARTESIAN_POINT ( 'NONE',  ( -6.782329983125267248, 10.49999999999999645, -105.0000000000000000 ) ) ;
#37201=EDGE_LOOP ( 'NONE', ( #27589, #37889, #8536, #21432, #23854, #47397 ) ) ;
#37204=CARTESIAN_POINT ( 'NONE',  ( 0.000000000000000000, 0.000000000000000000, 125.0000000000000000 ) ) ;
#37315=AXIS2_PLACEMENT_3D ( 'NONE', #42630, #9089, #27453 ) ;
#37318=CYLINDRICAL_SURFACE ( 'NONE', #12273, 11.59999999999999787 ) ;
#37344=CARTESIAN_POINT ( 'NONE',  ( -3.702536634196121224, 8.043911037661892749, -64.01812422950395387 ) ) ;
#37368=DIRECTION ( 'NONE',  ( 0.000000000000000000, 0.000000000000000000, 1.000000000000000000 ) ) ;
#37377=DIRECTION ( 'NONE',  ( 1.000000000000000000, 0.000000000000000000, -0.000000000000000000 ) ) ;
#37390=CIRCLE ( 'NONE', #6925, 11.59999999999999787 ) ;
#37413=PRODUCT_DEFINITION_FORMATION_WITH_SPECIFIED_SOURCE ( 'ANY', '', #36283, .NOT_KNOWN. ) ;
#37457=EDGE_LOOP ( 'NONE', ( #19960, #634, #24657, #27067 ) ) ;
#37460=ORIENTED_EDGE ( 'NONE', *, *, #12889, .T. ) ;
#37662=VERTEX_POINT ( 'NONE', #43008 ) ;
#37714=EDGE_CURVE ( 'NONE', #45171, #4936, #27853, .T. ) ;
#37716=DIRECTION ( 'NONE',  ( 0.6575728627325955200, -0.7533909544171996098, -1.230411769795008318E-16 ) ) ;
#37738=ADVANCED_FACE ( 'NONE', ( #46190 ), #42526, .T. ) ;
#37795=CARTESIAN_POINT ( 'NONE',  ( 0.000000000000000000, 0.000000000000000000, -54.99999999999998579 ) ) ;
#37796=CIRCLE ( 'NONE', #6561, 11.59999999999999787 ) ;
#37887=AXIS2_PLACEMENT_3D ( 'NONE', #39986, #10610, #21844 ) ;
#37889=ORIENTED_EDGE ( 'NONE', *, *, #28524, .T. ) ;
#37967=ORIENTED_EDGE ( 'NONE', *, *, #9390, .F. ) ;
#37977=FACE_OUTER_BOUND ( 'NONE', #31173, .T. ) ;
#38043=CARTESIAN_POINT ( 'NONE',  ( 0.000000000000000000, 0.000000000000000000, 40.80000000000001847 ) ) ;
#38123=DIRECTION ( 'NONE',  ( -1.000000000000000000, 0.000000000000000000, 0.000000000000000000 ) ) ;
#38132=LINE ( 'NONE', #4598, #14773 ) ;
#38275=DIRECTION ( 'NONE',  ( 0.000000000000000000, 0.000000000000000000, 1.000000000000000000 ) ) ;
#38286=DIRECTION ( 'NONE',  ( 1.000000000000000000, 0.000000000000000000, -0.000000000000000000 ) ) ;
#38355=CIRCLE ( 'NONE', #8640, 11.59999999999999787 ) ;
#38447=ORIENTED_EDGE ( 'NONE', *, *, #14385, .F. ) ;
#38454=CARTESIAN_POINT ( 'NONE',  ( 0.000000000000000000, 0.000000000000000000, -54.99999999999998579 ) ) ;
#38485=ORIENTED_EDGE ( 'NONE', *, *, #10987, .T. ) ;
#38492=ORIENTED_EDGE ( 'NONE', *, *, #22037, .F. ) ;
#38521=PLANE ( 'NONE',  #45845 ) ;
#38680=AXIS2_PLACEMENT_3D ( 'NONE', #6994, #33188, #36846 ) ;
#38721=AXIS2_PLACEMENT_3D ( 'NONE', #17032, #47605, #5790 ) ;
#38737=PRODUCT_CONTEXT ( 'NONE', #13219, 'mechanical' ) ;
#38766=ADVANCED_FACE ( 'NONE', ( #39466 ), #32122, .F. ) ;
#38774=DIRECTION ( 'NONE',  ( 0.000000000000000000, 0.000000000000000000, -1.000000000000000000 ) ) ;
#38780=DIRECTION ( 'NONE',  ( 1.000000000000000000, 0.000000000000000000, -0.000000000000000000 ) ) ;
#38818=CARTESIAN_POINT ( 'NONE',  ( -12.49999999999999645, 0.000000000000000000, -43.79999999999998295 ) ) ;
#38822=LINE ( 'NONE', #13577, #8326 ) ;
#38829=PLANE ( 'NONE',  #39320 ) ;
#38864=ORIENTED_EDGE ( 'NONE', *, *, #40369, .T. ) ;
#38928=ORIENTED_EDGE ( 'NONE', *, *, #19942, .F. ) ;
#38933=LINE ( 'NONE', #5390, #11403 ) ;
#38997=CARTESIAN_POINT ( 'NONE',  ( 6.782329983125267248, 10.49999999999999645, -105.0000000000000000 ) ) ;
#39027=EDGE_CURVE ( 'NONE', #37662, #36450, #40706, .T. ) ;
#39089=AXIS2_PLACEMENT_3D ( 'NONE', #2488, #10082, #24534 ) ;
#39117=AXIS2_PLACEMENT_3D ( 'NONE', #28192, #43609, #43131 ) ;
#39145=EDGE_CURVE ( 'NONE', #18977, #29688, #6340, .T. ) ;
#39252=DIRECTION ( 'NONE',  ( 0.000000000000000000, -1.000000000000000000, 0.000000000000000000 ) ) ;
#39256=CYLINDRICAL_SURFACE ( 'NONE', #43216, 11.59999999999999787 ) ;
#39270=ORIENTED_EDGE ( 'NONE', *, *, #2694, .F. ) ;
#39320=AXIS2_PLACEMENT_3D ( 'NONE', #12162, #35371, #23629 ) ;
#39328=DIRECTION ( 'NONE',  ( -0.000000000000000000, -0.000000000000000000, -1.000000000000000000 ) ) ;
#39357=VERTEX_POINT ( 'NONE', #38818 ) ;
#39360=ORIENTED_EDGE ( 'NONE', *, *, #43298, .T. ) ;
#39401=CARTESIAN_POINT ( 'NONE',  ( -7.469491406282116053, 4.756046723998915482, -45.00000000000000000 ) ) ;
#39466=FACE_OUTER_BOUND ( 'NONE', #17727, .T. ) ;
#39486=EDGE_CURVE ( 'NONE', #40640, #20736, #12615, .T. ) ;
#39549=PLANE ( 'NONE',  #48103 ) ;
#39560=AXIS2_PLACEMENT_3D ( 'NONE', #13216, #28138, #24461 ) ;
#39571=CARTESIAN_POINT ( 'NONE',  ( -12.49999999999999645, 0.000000000000000000, 53.20000000000001705 ) ) ;
#39674=CARTESIAN_POINT ( 'NONE',  ( 12.49999999999999645, 1.530808498934191127E-15, 53.20000000000001705 ) ) ;
#39742=DIRECTION ( 'NONE',  ( 0.000000000000000000, 0.000000000000000000, -1.000000000000000000 ) ) ;
#39766=ADVANCED_FACE ( 'NONE', ( #14783 ), #11107, .T. ) ;
#39780=VERTEX_POINT ( 'NONE', #30934 ) ;
#39793=DIRECTION ( 'NONE',  ( -8.090853898039828715E-17, 9.269810975720166919E-17, -1.000000000000000000 ) ) ;
#39804=ORIENTED_EDGE ( 'NONE', *, *, #3191, .F. ) ;
#39856=DIRECTION ( 'NONE',  ( 0.6575728627325957421, -0.7533909544171993877, -1.230411769795008318E-16 ) ) ;
#39861=DIRECTION ( 'NONE',  ( 0.7533909544171998318, 0.6575728627325954090, 0.000000000000000000 ) ) ;
#39933=ORIENTED_EDGE ( 'NONE', *, *, #12074, .T. ) ;
#39964=FACE_OUTER_BOUND ( 'NONE', #37201, .T. ) ;
#39986=CARTESIAN_POINT ( 'NONE',  ( 0.000000000000000000, 0.000000000000000000, 53.20000000000001705 ) ) ;
#39994=DIRECTION ( 'NONE',  ( 0.000000000000000000, 0.000000000000000000, 1.000000000000000000 ) ) ;
#40014=EDGE_LOOP ( 'NONE', ( #35191, #6886, #44256, #36376 ) ) ;
#40018=DIRECTION ( 'NONE',  ( 0.000000000000000000, 0.000000000000000000, 1.000000000000000000 ) ) ;
#40054=VECTOR ( 'NONE', #44030, 1000.000000000000000 ) ;
#40255=VECTOR ( 'NONE', #23037, 1000.000000000000000 ) ;
#40317=CARTESIAN_POINT ( 'NONE',  ( 0.000000000000000000, 0.000000000000000000, 40.80000000000001847 ) ) ;
#40353=ADVANCED_FACE ( 'NONE', ( #33601 ), #790, .T. ) ;
#40369=EDGE_CURVE ( 'NONE', #17350, #23067, #7895, .T. ) ;
#40389=DIRECTION ( 'NONE',  ( 8.090853898039833646E-17, -9.269810975720164453E-17, 1.000000000000000000 ) ) ;
#40396=DIRECTION ( 'NONE',  ( 0.6575728627325957421, -0.7533909544171993877, -1.230411769795008318E-16 ) ) ;
#40408=AXIS2_PLACEMENT_3D ( 'NONE', #12958, #17089, #8771 ) ;
#40438=ORIENTED_EDGE ( 'NONE', *, *, #47420, .F. ) ;
#40500=DIRECTION ( 'NONE',  ( -0.6575728627325955200, 0.7533909544171996098, 1.230411769795008318E-16 ) ) ;
#40583=DIRECTION ( 'NONE',  ( 1.000000000000000000, 0.000000000000000000, 0.000000000000000000 ) ) ;
#40630=ORIENTED_EDGE ( 'NONE', *, *, #20472, .F. ) ;
#40631=FACE_OUTER_BOUND ( 'NONE', #28311, .T. ) ;
#40640=VERTEX_POINT ( 'NONE', #36967 ) ;
#40697=VERTEX_POINT ( 'NONE', #14222 ) ;
#40706=CIRCLE ( 'NONE', #27451, 11.59999999999999787 ) ;
#40711=VECTOR ( 'NONE', #19559, 1000.000000000000114 ) ;
#40762=VECTOR ( 'NONE', #40500, 1000.000000000000114 ) ;
#40806=DIRECTION ( 'NONE',  ( 0.000000000000000000, 0.000000000000000000, 1.000000000000000000 ) ) ;
#40811=CARTESIAN_POINT ( 'NONE',  ( 11.59999999999999787, 1.420590287010929336E-15, 52.00000000000002132 ) ) ;
#40812=CARTESIAN_POINT ( 'NONE',  ( -7.469491406282094736, 4.756046723998911929, 32.98187577049606745 ) ) ;
#40872=FILL_AREA_STYLE ('',( #33034 ) ) ;
#40889=ORIENTED_EDGE ( 'NONE', *, *, #7050, .F. ) ;
#40925=DIRECTION ( 'NONE',  ( 0.000000000000000000, 0.000000000000000000, 1.000000000000000000 ) ) ;
#40927=DIRECTION ( 'NONE',  ( -0.000000000000000000, -0.000000000000000000, -1.000000000000000000 ) ) ;
#40960=EDGE_CURVE ( 'NONE', #19441, #26557, #1473, .T. ) ;
#40992=CARTESIAN_POINT ( 'NONE',  ( -3.702536634196119447, 8.043911037661890973, -45.00000000000000000 ) ) ;
#40998=DIRECTION ( 'NONE',  ( 1.000000000000000000, 0.000000000000000000, 0.000000000000000000 ) ) ;
#41040=EDGE_CURVE ( 'NONE', #27843, #8199, #21950, .T. ) ;
#41176=ORIENTED_EDGE ( 'NONE', *, *, #7995, .F. ) ;
#41362=CARTESIAN_POINT ( 'NONE',  ( -12.49999999999999645, 0.000000000000000000, -56.19999999999998863 ) ) ;
#41367=CARTESIAN_POINT ( 'NONE',  ( 6.782329983125267248, 10.49999999999999645, -125.0000000000000000 ) ) ;
#41382=VECTOR ( 'NONE', #3716, 1000.000000000000000 ) ;
#41399=LINE ( 'NONE', #29417, #31345 ) ;
#41458=AXIS2_PLACEMENT_3D ( 'NONE', #10646, #28759, #47369 ) ;
#41464=ORIENTED_EDGE ( 'NONE', *, *, #40369, .F. ) ;
#41597=AXIS2_PLACEMENT_3D ( 'NONE', #3142, #10507, #29094 ) ;
#41629=VERTEX_POINT ( 'NONE', #7245 ) ;
#41684=VECTOR ( 'NONE', #5923, 1000.000000000000000 ) ;
#41696=AXIS2_PLACEMENT_3D ( 'NONE', #22311, #16128, #42298 ) ;
#41902=CIRCLE ( 'NONE', #1260, 12.49999999999999645 ) ;
#41915=DIRECTION ( 'NONE',  ( 1.000000000000000000, 0.000000000000000000, 0.000000000000000000 ) ) ;
#41977=DIRECTION ( 'NONE',  ( -1.000000000000000000, 0.000000000000000000, 0.000000000000000000 ) ) ;
#42020=ORIENTED_EDGE ( 'NONE', *, *, #12655, .T. ) ;
#42046=EDGE_CURVE ( 'NONE', #23067, #1692, #9540, .T. ) ;
#42063=EDGE_CURVE ( 'NONE', #39780, #1692, #22309, .T. ) ;
#42086=DIRECTION ( 'NONE',  ( -1.000000000000000000, 0.000000000000000000, 0.000000000000000000 ) ) ;
#42117=ORIENTED_EDGE ( 'NONE', *, *, #20163, .F. ) ;
#42151=ORIENTED_EDGE ( 'NONE', *, *, #30554, .F. ) ;
#42175=DIRECTION ( 'NONE',  ( 1.000000000000000000, 0.000000000000000000, 0.000000000000000000 ) ) ;
#42202=ADVANCED_FACE ( 'NONE', ( #19818 ), #1719, .T. ) ;
#42232=EDGE_CURVE ( 'NONE', #34023, #19441, #36202, .T. ) ;
#42290=VERTEX_POINT ( 'NONE', #43326 ) ;
#42298=DIRECTION ( 'NONE',  ( 1.000000000000000000, 0.000000000000000000, 0.000000000000000000 ) ) ;
#42321=ORIENTED_EDGE ( 'NONE', *, *, #7786, .F. ) ;
#42371=EDGE_CURVE ( 'NONE', #34724, #6953, #36169, .T. ) ;
#42448=AXIS2_PLACEMENT_3D ( 'NONE', #16502, #35097, #2069 ) ;
#42466=CIRCLE ( 'NONE', #33864, 11.59999999999999787 ) ;
#42526=CYLINDRICAL_SURFACE ( 'NONE', #28114, 12.49999999999999645 ) ;
#42553=CARTESIAN_POINT ( 'NONE',  ( 0.000000000000000000, 0.000000000000000000, 53.20000000000001705 ) ) ;
#42586=CIRCLE ( 'NONE', #38680, 12.49999999999999645 ) ;
#42615=ADVANCED_FACE ( 'NONE', ( #14126 ), #32957, .T. ) ;
#42626=LINE ( 'NONE', #30889, #21627 ) ;
#42630=CARTESIAN_POINT ( 'NONE',  ( 0.000000000000000000, 0.000000000000000000, -56.19999999999998863 ) ) ;
#42644=SHAPE_DEFINITION_REPRESENTATION ( #8582, #2782 ) ;
#42703=FACE_OUTER_BOUND ( 'NONE', #2905, .T. ) ;
#42717=DIRECTION ( 'NONE',  ( -0.000000000000000000, -0.000000000000000000, -1.000000000000000000 ) ) ;
#42821=CIRCLE ( 'NONE', #4519, 12.49999999999999645 ) ;
#42876=ORIENTED_EDGE ( 'NONE', *, *, #10984, .T. ) ;
#42897=ORIENTED_EDGE ( 'NONE', *, *, #22490, .T. ) ;
#42921=STYLED_ITEM ( 'NONE', ( #18598 ), #1820 ) ;
#42938=ORIENTED_EDGE ( 'NONE', *, *, #18304, .T. ) ;
#42984=ADVANCED_FACE ( 'NONE', ( #46161 ), #38829, .F. ) ;
#42999=VERTEX_POINT ( 'NONE', #4796 ) ;
#43008=CARTESIAN_POINT ( 'NONE',  ( -11.59999999999999787, 0.000000000000000000, 40.80000000000001847 ) ) ;
#43028=ORIENTED_EDGE ( 'NONE', *, *, #14053, .F. ) ;
#43050=FACE_OUTER_BOUND ( 'NONE', #46564, .T. ) ;
#43131=DIRECTION ( 'NONE',  ( 1.000000000000000000, 0.000000000000000000, -0.000000000000000000 ) ) ;
#43194=ORIENTED_EDGE ( 'NONE', *, *, #19993, .F. ) ;
#43198=DIRECTION ( 'NONE',  ( 0.7533909544171997208, 0.6575728627325955200, 0.000000000000000000 ) ) ;
#43216=AXIS2_PLACEMENT_3D ( 'NONE', #5730, #32163, #5487 ) ;
#43244=AXIS2_PLACEMENT_3D ( 'NONE', #15006, #44857, #3241 ) ;
#43298=EDGE_CURVE ( 'NONE', #43965, #1594, #45871, .T. ) ;
#43326=CARTESIAN_POINT ( 'NONE',  ( 12.49999999999999645, 1.530808498934191127E-15, -44.99999999999998579 ) ) ;
#43331=ORIENTED_EDGE ( 'NONE', *, *, #24323, .T. ) ;
#43355=CARTESIAN_POINT ( 'NONE',  ( 0.000000000000000000, 0.000000000000000000, -125.0000000000000000 ) ) ;
#43407=DIRECTION ( 'NONE',  ( -1.000000000000000000, 0.000000000000000000, 0.000000000000000000 ) ) ;
#43424=VECTOR ( 'NONE', #4679, 1000.000000000000000 ) ;
#43430=DIRECTION ( 'NONE',  ( 1.000000000000000000, 0.000000000000000000, -0.000000000000000000 ) ) ;
#43447=ORIENTED_EDGE ( 'NONE', *, *, #19696, .F. ) ;
#43456=EDGE_CURVE ( 'NONE', #9518, #4524, #35512, .T. ) ;
#43530=CARTESIAN_POINT ( 'NONE',  ( -9.332068499558246799, 6.890028847512375876, 42.00000000000001421 ) ) ;
#43594=VECTOR ( 'NONE', #48153, 1000.000000000000000 ) ;
#43609=DIRECTION ( 'NONE',  ( 0.000000000000000000, 0.000000000000000000, 1.000000000000000000 ) ) ;
#43610=ORIENTED_EDGE ( 'NONE', *, *, #9390, .T. ) ;
#43619=FACE_OUTER_BOUND ( 'NONE', #25082, .T. ) ;
#43670=ORIENTED_EDGE ( 'NONE', *, *, #37714, .T. ) ;
#43683=CARTESIAN_POINT ( 'NONE',  ( 0.000000000000000000, 0.000000000000000000, 52.00000000000002132 ) ) ;
#43765=ORIENTED_EDGE ( 'NONE', *, *, #170, .T. ) ;
#43795=CARTESIAN_POINT ( 'NONE',  ( -12.49999999999999645, 0.000000000000000000, 40.80000000000001847 ) ) ;
#43798=CIRCLE ( 'NONE', #21914, 11.59999999999999787 ) ;
#43871=AXIS2_PLACEMENT_3D ( 'NONE', #29656, #40925, #22328 ) ;
#43885=EDGE_CURVE ( 'NONE', #34724, #37662, #15547, .T. ) ;
#43893=ORIENTED_EDGE ( 'NONE', *, *, #20894, .F. ) ;
#43900=CIRCLE ( 'NONE', #28284, 12.49999999999999645 ) ;
#43910=LINE ( 'NONE', #32428, #12429 ) ;
#43965=VERTEX_POINT ( 'NONE', #32435 ) ;
#43981=DIRECTION ( 'NONE',  ( 0.000000000000000000, 0.000000000000000000, -1.000000000000000000 ) ) ;
#43994=DIRECTION ( 'NONE',  ( -0.6575728627325957421, 0.7533909544171993877, 1.230411769795008318E-16 ) ) ;
#43995=ADVANCED_FACE ( 'NONE', ( #24350 ), #27808, .T. ) ;
#44019=AXIS2_PLACEMENT_3D ( 'NONE', #28350, #39861, #21236 ) ;
#44028=ADVANCED_FACE ( 'NONE', ( #17485 ), #5516, .T. ) ;
#44030=DIRECTION ( 'NONE',  ( 8.090853898039828715E-17, -9.269810975720166919E-17, 1.000000000000000000 ) ) ;
#44037=VECTOR ( 'NONE', #39856, 1000.000000000000114 ) ;
#44073=VECTOR ( 'NONE', #25671, 1000.000000000000000 ) ;
#44097=FACE_OUTER_BOUND ( 'NONE', #31267, .T. ) ;
#44225=CARTESIAN_POINT ( 'NONE',  ( -8.637688417678548447, 13.69818742750669749, -55.00000000000000000 ) ) ;
#44249=FACE_OUTER_BOUND ( 'NONE', #40014, .T. ) ;
#44256=ORIENTED_EDGE ( 'NONE', *, *, #25125, .T. ) ;
#44355=LINE ( 'NONE', #21827, #46198 ) ;
#44419=CARTESIAN_POINT ( 'NONE',  ( 0.000000000000000000, 0.000000000000000000, 42.00000000000001421 ) ) ;
#44439=ORIENTED_EDGE ( 'NONE', *, *, #10186, .T. ) ;
#44515=AXIS2_PLACEMENT_3D ( 'NONE', #36751, #36285, #17682 ) ;
#44534=DIRECTION ( 'NONE',  ( -0.7533909544171994987, -0.6575728627325958531, 2.465190328815662439E-32 ) ) ;
#44554=FACE_OUTER_BOUND ( 'NONE', #14325, .T. ) ;
#44570=VERTEX_POINT ( 'NONE', #47532 ) ;
#44588=LINE ( 'NONE', #36995, #41382 ) ;
#44591=ADVANCED_FACE ( 'NONE', ( #39964 ), #18400, .T. ) ;
#44600=CIRCLE ( 'NONE', #41458, 12.49999999999999645 ) ;
#44717=DIRECTION ( 'NONE',  ( 1.000000000000000000, 0.000000000000000000, 0.000000000000000000 ) ) ;
#44734=EDGE_CURVE ( 'NONE', #46550, #31057, #4453, .T. ) ;
#44789=ORIENTED_EDGE ( 'NONE', *, *, #22037, .T. ) ;
#44848=ORIENTED_EDGE ( 'NONE', *, *, #41040, .F. ) ;
#44851=VECTOR ( 'NONE', #10405, 1000.000000000000000 ) ;
#44857=DIRECTION ( 'NONE',  ( -0.7533909544171996098, -0.6575728627325956310, 0.000000000000000000 ) ) ;
#44865=CIRCLE ( 'NONE', #21417, 11.59999999999999787 ) ;
#44866=AXIS2_PLACEMENT_3D ( 'NONE', #33333, #48261, #2980 ) ;
#44912=VECTOR ( 'NONE', #18722, 1000.000000000000000 ) ;
#44986=ADVANCED_FACE ( 'NONE', ( #3156 ), #17614, .F. ) ;
#45006=ORIENTED_EDGE ( 'NONE', *, *, #4983, .T. ) ;
#45090=CARTESIAN_POINT ( 'NONE',  ( 0.000000000000000000, 0.000000000000000000, -43.79999999999998295 ) ) ;
#45171=VERTEX_POINT ( 'NONE', #18809 ) ;
#45180=ORIENTED_EDGE ( 'NONE', *, *, #10060, .T. ) ;
#45285=VECTOR ( 'NONE', #40927, 1000.000000000000000 ) ;
#45307=DIRECTION ( 'NONE',  ( -1.000000000000000000, 0.000000000000000000, 0.000000000000000000 ) ) ;
#45381=CARTESIAN_POINT ( 'NONE',  ( 6.782329983125267248, 10.49999999999999645, -105.0000000000000000 ) ) ;
#45395=CIRCLE ( 'NONE', #12603, 11.59999999999999787 ) ;
#45707=ORIENTED_EDGE ( 'NONE', *, *, #16425, .F. ) ;
#45733=ORIENTED_EDGE ( 'NONE', *, *, #10789, .T. ) ;
#45816=DIRECTION ( 'NONE',  ( -0.000000000000000000, -0.000000000000000000, -1.000000000000000000 ) ) ;
#45845=AXIS2_PLACEMENT_3D ( 'NONE', #38043, #38275, #38780 ) ;
#45871=LINE ( 'NONE', #12814, #8880 ) ;
#45886=ORIENTED_EDGE ( 'NONE', *, *, #42232, .F. ) ;
#46161=FACE_OUTER_BOUND ( 'NONE', #2546, .T. ) ;
#46190=FACE_OUTER_BOUND ( 'NONE', #1636, .T. ) ;
#46198=VECTOR ( 'NONE', #7393, 1000.000000000000000 ) ;
#46206=ADVANCED_FACE ( 'NONE', ( #47957 ), #3405, .F. ) ;
#46262=ORIENTED_EDGE ( 'NONE', *, *, #26987, .F. ) ;
#46291=LINE ( 'NONE', #4926, #9885 ) ;
#46304=VERTEX_POINT ( 'NONE', #13728 ) ;
#46350=CARTESIAN_POINT ( 'NONE',  ( -9.937067298023309903, 7.583184918921312523, 42.00000000000001421 ) ) ;
#46379=VECTOR ( 'NONE', #46412, 1000.000000000000000 ) ;
#46406=LINE ( 'NONE', #24847, #33756 ) ;
#46409=EDGE_LOOP ( 'NONE', ( #28931, #14000, #40438, #26108 ) ) ;
#46412=DIRECTION ( 'NONE',  ( -0.6575728627325957421, 0.7533909544171994987, 0.000000000000000000 ) ) ;
#46550=VERTEX_POINT ( 'NONE', #31815 ) ;
#46558=EDGE_CURVE ( 'NONE', #17326, #31057, #5998, .T. ) ;
#46564=EDGE_LOOP ( 'NONE', ( #20470, #7373, #25518, #11237, #16162, #42117 ) ) ;
#46588=ORIENTED_EDGE ( 'NONE', *, *, #39027, .T. ) ;
#46605=DIRECTION ( 'NONE',  ( -1.000000000000000000, 0.000000000000000000, 0.000000000000000000 ) ) ;
#46645=DIRECTION ( 'NONE',  ( -0.000000000000000000, -0.000000000000000000, -1.000000000000000000 ) ) ;
#46727=VERTEX_POINT ( 'NONE', #43530 ) ;
#46824=VERTEX_POINT ( 'NONE', #40811 ) ;
#46883=DIRECTION ( 'NONE',  ( -0.6575728627325955200, 0.7533909544171996098, 1.230411769795008318E-16 ) ) ;
#46930=ORIENTED_EDGE ( 'NONE', *, *, #31903, .F. ) ;
#46947=VECTOR ( 'NONE', #34891, 1000.000000000000000 ) ;
#46960=CARTESIAN_POINT ( 'NONE',  ( -11.59999999999999787, 0.000000000000000000, -44.99999999999998579 ) ) ;
#46972=AXIS2_PLACEMENT_3D ( 'NONE', #40317, #47631, #2849 ) ;
#46999=CARTESIAN_POINT ( 'NONE',  ( -12.49999999999999645, 0.000000000000000000, -54.99999999999998579 ) ) ;
#47034=ORIENTED_EDGE ( 'NONE', *, *, #34301, .F. ) ;
#47054=EDGE_LOOP ( 'NONE', ( #35306, #20314 ) ) ;
#47076=ORIENTED_EDGE ( 'NONE', *, *, #22083, .T. ) ;
#47081=AXIS2_PLACEMENT_3D ( 'NONE', #26952, #18624, #15448 ) ;
#47300=ORIENTED_EDGE ( 'NONE', *, *, #10743, .F. ) ;
#47342=ORIENTED_EDGE ( 'NONE', *, *, #39145, .T. ) ;
#47369=DIRECTION ( 'NONE',  ( 1.000000000000000000, 0.000000000000000000, 0.000000000000000000 ) ) ;
#47370=ADVANCED_FACE ( 'NONE', ( #23351 ), #12354, .T. ) ;
#47397=ORIENTED_EDGE ( 'NONE', *, *, #14426, .F. ) ;
#47420=EDGE_CURVE ( 'NONE', #44570, #15125, #42821, .T. ) ;
#47444=VECTOR ( 'NONE', #1389, 1000.000000000000000 ) ;
#47445=DIRECTION ( 'NONE',  ( 0.000000000000000000, 0.000000000000000000, 1.000000000000000000 ) ) ;
#47479=CARTESIAN_POINT ( 'NONE',  ( 0.000000000000000000, 0.000000000000000000, -54.99999999999998579 ) ) ;
#47486=DIRECTION ( 'NONE',  ( 0.000000000000000000, 0.000000000000000000, 1.000000000000000000 ) ) ;
#47490=SHAPE_REPRESENTATION_RELATIONSHIP ( 'NONE' , 'NONE' ,  #2782, #1820 ) ;
#47499=ORIENTED_EDGE ( 'NONE', *, *, #31067, .F. ) ;
#47506=EDGE_CURVE ( 'NONE', #19563, #36269, #18354, .T. ) ;
#47532=CARTESIAN_POINT ( 'NONE',  ( -12.49999999999999645, 0.000000000000000000, -125.0000000000000000 ) ) ;
#47583=LINE ( 'NONE', #13583, #40762 ) ;
#47605=DIRECTION ( 'NONE',  ( -0.000000000000000000, -0.000000000000000000, -1.000000000000000000 ) ) ;
#47627=ORIENTED_EDGE ( 'NONE', *, *, #42063, .T. ) ;
#47631=DIRECTION ( 'NONE',  ( 0.000000000000000000, 0.000000000000000000, 1.000000000000000000 ) ) ;
#47677=DIRECTION ( 'NONE',  ( 1.000000000000000000, 0.000000000000000000, 0.000000000000000000 ) ) ;
#47712=EDGE_CURVE ( 'NONE', #16632, #46304, #19073, .T. ) ;
#47713=CARTESIAN_POINT ( 'NONE',  ( -3.702536634196095910, 8.043911037661889196, 32.98187577049606745 ) ) ;
#47720=CARTESIAN_POINT ( 'NONE',  ( -7.469491406282094736, 4.756046723998911929, 42.00000000000001421 ) ) ;
#47731=PLANE ( 'NONE',  #26076 ) ;
#47849=EDGE_LOOP ( 'NONE', ( #1971, #42020 ) ) ;
#47886=DIRECTION ( 'NONE',  ( 1.000000000000000000, 0.000000000000000000, 0.000000000000000000 ) ) ;
#47894=DIRECTION ( 'NONE',  ( 1.000000000000000000, 0.000000000000000000, 0.000000000000000000 ) ) ;
#47938=AXIS2_PLACEMENT_3D ( 'NONE', #13750, #13499, #9107 ) ;
#47954=FACE_OUTER_BOUND ( 'NONE', #37457, .T. ) ;
#47957=FACE_OUTER_BOUND ( 'NONE', #19403, .T. ) ;
#47963=SURFACE_STYLE_FILL_AREA ( #40872 ) ;
#48000=ORIENTED_EDGE ( 'NONE', *, *, #46558, .T. ) ;
#48015=LINE ( 'NONE', #21347, #45285 ) ;
#48024=DIRECTION ( 'NONE',  ( -1.000000000000000000, 0.000000000000000000, 0.000000000000000000 ) ) ;
#48050=EDGE_CURVE ( 'NONE', #43965, #9118, #37390, .T. ) ;
#48070=ORIENTED_EDGE ( 'NONE', *, *, #19942, .T. ) ;
#48103=AXIS2_PLACEMENT_3D ( 'NONE', #20932, #20684, #6244 ) ;
#48122=ORIENTED_EDGE ( 'NONE', *, *, #31903, .T. ) ;
#48150=CARTESIAN_POINT ( 'NONE',  ( 0.000000000000000000, 0.000000000000000000, -54.99999999999998579 ) ) ;
#48153=DIRECTION ( 'NONE',  ( -0.000000000000000000, -0.000000000000000000, -1.000000000000000000 ) ) ;
#48177=EDGE_CURVE ( 'NONE', #14712, #19563, #28945, .T. ) ;
#48247=ORIENTED_EDGE ( 'NONE', *, *, #20472, .T. ) ;
#48261=DIRECTION ( 'NONE',  ( 0.000000000000000000, 0.000000000000000000, -1.000000000000000000 ) ) ;
#48262=CYLINDRICAL_SURFACE ( 'NONE', #17995, 11.59999999999999787 ) ;
#48373=LINE ( 'NONE', #14853, #21180 ) ;
#48447=( NAMED_UNIT ( * ) PLANE_ANGLE_UNIT ( ) SI_UNIT ( $, .RADIAN. ) );
ENDSEC;
END-ISO-10303-21;
